ISO-10303-21;
HEADER;
FILE_DESCRIPTION (('STEP AP203'),
    '1' );
FILE_NAME ('1602p_c_36.step',
    '2026-10-31T14:11:27',
    ( '' ),
    ( '' ),
    'SwSTEP 2.0',
    'SolidWorks 2024',
    '' );
FILE_SCHEMA (( 'AUTOMOTIVE_DESIGN' ));
ENDSEC;

DATA;
#2=DIRECTION ( 'NONE',  ( -0.9730401042858035643, 0.2306359803922028717, 5.958148513035547083E-17 ) ) ;
#12=CARTESIAN_POINT ( 'NONE',  ( 35.59419854219520118, 9.774809681453518806, 20.00000000000000000 ) ) ;
#18=CARTESIAN_POINT ( 'NONE',  ( 33.99815084691889666, 11.09517226956036673, 8.954072598562477836 ) ) ;
#76=ORIENTED_EDGE ( 'NONE', *, *, #8643, .T. ) ;
#94=EDGE_CURVE ( 'NONE', #17862, #6798, #19506, .T. ) ;
#101=CIRCLE ( 'NONE', #2773, 2.066999999999999282 ) ;
#106=DIRECTION ( 'NONE',  ( -0.9730401042858035643, 0.2306359803922028717, 5.958148513035547083E-17 ) ) ;
#142=VERTEX_POINT ( 'NONE', #16617 ) ;
#144=CARTESIAN_POINT ( 'NONE',  ( 34.27408172216480153, 8.178586146432554216, 8.806355889830941308 ) ) ;
#176=CARTESIAN_POINT ( 'NONE',  ( 36.18988576660174061, 7.790900190088850152, -8.819913685435235351 ) ) ;
#189=CYLINDRICAL_SURFACE ( 'NONE', #19053, 2.750000000000000000 ) ;
#199=VERTEX_POINT ( 'NONE', #2140 ) ;
#249=EDGE_CURVE ( 'NONE', #9426, #18548, #22088, .T. ) ;
#270=CARTESIAN_POINT ( 'NONE',  ( 35.06754128096959988, 7.552872603316886035, 19.78350000000001074 ) ) ;
#280=ORIENTED_EDGE ( 'NONE', *, *, #13563, .F. ) ;
#298=CIRCLE ( 'NONE', #13970, 5.000000000000004441 ) ;
#317=FACE_BOUND ( 'NONE', #5832, .T. ) ;
#325=DIRECTION ( 'NONE',  ( -0.2306359803922010121, -0.9730401042858040084, 0.000000000000000000 ) ) ;
#361=LINE ( 'NONE', #2404, #15555 ) ;
#374=CARTESIAN_POINT ( 'NONE',  ( 34.41917370704140211, 26.49663125198719982, -20.00000000000029843 ) ) ;
#385=EDGE_CURVE ( 'NONE', #9841, #20204, #20766, .T. ) ;
#393=DIRECTION ( 'NONE',  ( 0.1630842657209330415, 0.6880432561069529385, -0.7071067811865519026 ) ) ;
#394=DIRECTION ( 'NONE',  ( -0.2306359803922009288, -0.9730401042858040084, 0.000000000000000000 ) ) ;
#396=CARTESIAN_POINT ( 'NONE',  ( 32.12387896813558541, -7.901357381965649296, -13.00000000000000000 ) ) ;
#415=DIRECTION ( 'NONE',  ( 1.000000000000000000, 0.000000000000000000, 0.000000000000000000 ) ) ;
#427=AXIS2_PLACEMENT_3D ( 'NONE', #20536, #16853, #578 ) ;
#516=DIRECTION ( 'NONE',  ( -0.1630842657209334579, -0.6880432561069538266, 0.7071067811865507924 ) ) ;
#517=EDGE_CURVE ( 'NONE', #3272, #20682, #5535, .T. ) ;
#536=ORIENTED_EDGE ( 'NONE', *, *, #21834, .F. ) ;
#538=ORIENTED_EDGE ( 'NONE', *, *, #17504, .F. ) ;
#572=CARTESIAN_POINT ( 'NONE',  ( 35.59419854219520118, 9.774809681453518806, 19.56700000000000017 ) ) ;
#578=DIRECTION ( 'NONE',  ( -0.2306359803922033158, -0.9730401042858034533, 0.000000000000000000 ) ) ;
#580=CARTESIAN_POINT ( 'NONE',  ( 27.73073027566755044, -1.721531772301079899, -13.00000000000000000 ) ) ;
#586=CARTESIAN_POINT ( 'NONE',  ( 33.27705887009660302, -3.036156860536515012, 13.00000000000000000 ) ) ;
#645=VERTEX_POINT ( 'NONE', #21913 ) ;
#692=ORIENTED_EDGE ( 'NONE', *, *, #5300, .T. ) ;
#694=CARTESIAN_POINT ( 'NONE',  ( 35.59419854219520118, 9.774809681453239918, -37.44562646538079775 ) ) ;
#696=CARTESIAN_POINT ( 'NONE',  ( 33.27705887009660302, -3.036156860536499913, 13.00000000000000000 ) ) ;
#708=LINE ( 'NONE', #17109, #7822 ) ;
#711=EDGE_LOOP ( 'NONE', ( #16585, #16731 ) ) ;
#716=ORIENTED_EDGE ( 'NONE', *, *, #13563, .T. ) ;
#717=DIRECTION ( 'NONE',  ( -0.2306359803922010121, -0.9730401042858040084, 0.000000000000000000 ) ) ;
#731=CIRCLE ( 'NONE', #13652, 2.750000000000001332 ) ;
#733=VECTOR ( 'NONE', #8527, 999.9999999999998863 ) ;
#737=DIRECTION ( 'NONE',  ( -0.9730401042858036753, 0.2306359803922028995, 5.958148513035547083E-17 ) ) ;
#768=LINE ( 'NONE', #15389, #14688 ) ;
#773=CARTESIAN_POINT ( 'NONE',  ( 34.98595693676443830, 7.794708766260042943, -8.759424124906628251 ) ) ;
#785=CARTESIAN_POINT ( 'NONE',  ( 26.57755037370655060, -6.586732293730130472, -18.00000000000000000 ) ) ;
#814=CARTESIAN_POINT ( 'NONE',  ( 35.59419854219520118, 9.774809681453319854, -20.00000000000000000 ) ) ;
#829=AXIS2_PLACEMENT_3D ( 'NONE', #12501, #11670, #16865 ) ;
#836=CARTESIAN_POINT ( 'NONE',  ( 34.43023877205762062, 1.829043660892520684, 13.00000000000000000 ) ) ;
#854=VECTOR ( 'NONE', #2228, 999.9999999999998863 ) ;
#876=CARTESIAN_POINT ( 'NONE',  ( 33.72726576586480007, 23.57751093912980167, -13.00000000000030020 ) ) ;
#942=ORIENTED_EDGE ( 'NONE', *, *, #11617, .F. ) ;
#993=DIRECTION ( 'NONE',  ( -0.2306359803922033158, -0.9730401042858034533, 0.000000000000000000 ) ) ;
#1020=CARTESIAN_POINT ( 'NONE',  ( 33.27705887009660302, -3.036156860536630031, -13.00000000000000000 ) ) ;
#1034=EDGE_LOOP ( 'NONE', ( #6117, #22983, #18814, #12355 ) ) ;
#1079=DIRECTION ( 'NONE',  ( -0.2306359803922033713, -0.9730401042858034533, 4.558064749665356219E-15 ) ) ;
#1094=CARTESIAN_POINT ( 'NONE',  ( 36.69650084708651150, 11.52859305909626286, 8.783982963266916855 ) ) ;
#1097=EDGE_CURVE ( 'NONE', #11267, #11726, #12532, .T. ) ;
#1098=DIRECTION ( 'NONE',  ( -0.2306359803922033436, -0.9730401042858034533, 0.000000000000000000 ) ) ;
#1105=EDGE_LOOP ( 'NONE', ( #15851, #7040, #21791, #2059 ) ) ;
#1130=CARTESIAN_POINT ( 'NONE',  ( 34.28006175981952453, 11.39274844856495683, -8.911849358505339325 ) ) ;
#1134=ADVANCED_FACE ( 'NONE', ( #11112, #5738 ), #16898, .T. ) ;
#1141=DIRECTION ( 'NONE',  ( 0.1630842657209329583, 0.6880432561069529385, -0.7071067811865517916 ) ) ;
#1144=EDGE_CURVE ( 'NONE', #6181, #10197, #4838, .T. ) ;
#1163=DIRECTION ( 'NONE',  ( -0.9730401042858035643, 0.2306359803922028717, 5.958148513035547083E-17 ) ) ;
#1168=ORIENTED_EDGE ( 'NONE', *, *, #12424, .T. ) ;
#1169=AXIS2_PLACEMENT_3D ( 'NONE', #22497, #5878, #22361 ) ;
#1181=LINE ( 'NONE', #8796, #9614 ) ;
#1193=CARTESIAN_POINT ( 'NONE',  ( 34.88044566782586031, 28.44271146055899990, 12.99999999999979927 ) ) ;
#1199=DIRECTION ( 'NONE',  ( -0.1630842657209329027, -0.6880432561069529385, 0.7071067811865519026 ) ) ;
#1215=CARTESIAN_POINT ( 'NONE',  ( 36.91588945311071512, 11.36978919325550308, 8.806536740235856087 ) ) ;
#1227=ORIENTED_EDGE ( 'NONE', *, *, #249, .T. ) ;
#1234=ORIENTED_EDGE ( 'NONE', *, *, #17100, .T. ) ;
#1259=CARTESIAN_POINT ( 'NONE',  ( 33.77164795278312681, 10.75935922908529996, -8.984920035094603463 ) ) ;
#1285=EDGE_LOOP ( 'NONE', ( #14029, #10903, #7991, #3682 ) ) ;
#1310=ORIENTED_EDGE ( 'NONE', *, *, #12767, .T. ) ;
#1314=LINE ( 'NONE', #8581, #17932 ) ;
#1327=FACE_OUTER_BOUND ( 'NONE', #2460, .T. ) ;
#1332=CARTESIAN_POINT ( 'NONE',  ( 35.65672502062392368, 7.704309056808580358, 8.774947752588879268 ) ) ;
#1343=DIRECTION ( 'NONE',  ( 0.2306359803922017615, 0.9730401042858037863, -3.356987858687580135E-15 ) ) ;
#1359=CARTESIAN_POINT ( 'NONE',  ( 36.30795141656459890, -8.893092097651951633, 18.00000000000000000 ) ) ;
#1396=VERTEX_POINT ( 'NONE', #8236 ) ;
#1407=ORIENTED_EDGE ( 'NONE', *, *, #18710, .T. ) ;
#1409=CARTESIAN_POINT ( 'NONE',  ( 38.63934541421534874, 19.58702556410829487, -13.00000000000029665 ) ) ;
#1412=EDGE_CURVE ( 'NONE', #4600, #645, #1790, .T. ) ;
#1414=AXIS2_PLACEMENT_3D ( 'NONE', #10896, #18361, #5170 ) ;
#1437=FACE_OUTER_BOUND ( 'NONE', #12122, .T. ) ;
#1479=CARTESIAN_POINT ( 'NONE',  ( 34.62304412778976825, 11.60439875761490747, -8.864945788362616597 ) ) ;
#1508=EDGE_CURVE ( 'NONE', #10900, #22391, #8479, .T. ) ;
#1522=DIRECTION ( 'NONE',  ( -0.9730401042858035643, 0.2306359803922028717, 5.958148513035547083E-17 ) ) ;
#1545=CARTESIAN_POINT ( 'NONE',  ( 45.07211867146829576, 28.08243186520855161, 15.99999999999969802 ) ) ;
#1560=EDGE_CURVE ( 'NONE', #10900, #21046, #7052, .T. ) ;
#1571=ADVANCED_FACE ( 'NONE', ( #1327, #8828 ), #23297, .T. ) ;
#1573=VERTEX_POINT ( 'NONE', #17845 ) ;
#1596=DIRECTION ( 'NONE',  ( 0.9730401042858035643, -0.2306359803922028717, -5.958148513035547083E-17 ) ) ;
#1600=LINE ( 'NONE', #21089, #733 ) ;
#1609=VERTEX_POINT ( 'NONE', #6808 ) ;
#1629=VECTOR ( 'NONE', #7769, 1000.000000000000114 ) ;
#1634=VECTOR ( 'NONE', #15146, 999.9999999999998863 ) ;
#1664=PLANE ( 'NONE',  #13759 ) ;
#1670=EDGE_CURVE ( 'NONE', #19937, #21288, #7163, .T. ) ;
#1683=EDGE_CURVE ( 'NONE', #13022, #13532, #20116, .T. ) ;
#1729=EDGE_CURVE ( 'NONE', #9507, #22544, #12846, .T. ) ;
#1746=AXIS2_PLACEMENT_3D ( 'NONE', #2505, #18903, #22446 ) ;
#1747=CIRCLE ( 'NONE', #22616, 5.000000000000001776 ) ;
#1790=CIRCLE ( 'NONE', #15071, 2.066999999999999282 ) ;
#1806=ORIENTED_EDGE ( 'NONE', *, *, #10576, .F. ) ;
#1808=CARTESIAN_POINT ( 'NONE',  ( 34.73651500123170166, 11.67452289462551285, 8.849422422067890537 ) ) ;
#1816=ORIENTED_EDGE ( 'NONE', *, *, #16620, .T. ) ;
#1880=CARTESIAN_POINT ( 'NONE',  ( 45.07211867146820339, 28.08243186520834911, -20.00000000000029843 ) ) ;
#1924=CARTESIAN_POINT ( 'NONE',  ( 33.76470586405379493, 8.803418887774272505, 8.896078739569134086 ) ) ;
#1945=EDGE_CURVE ( 'NONE', #17998, #6181, #708, .T. ) ;
#1949=CARTESIAN_POINT ( 'NONE',  ( 35.59419854219520118, 9.774809681453518806, 20.00000000000000000 ) ) ;
#1958=CARTESIAN_POINT ( 'NONE',  ( 39.27359436029389883, 22.26288585089439920, 12.99999999999970157 ) ) ;
#1968=CARTESIAN_POINT ( 'NONE',  ( 36.56362820255242241, 7.944277063050280141, -8.864716985163925145 ) ) ;
#1974=ADVANCED_FACE ( 'NONE', ( #15208 ), #10013, .F. ) ;
#1981=VERTEX_POINT ( 'NONE', #11786 ) ;
#1983=AXIS2_PLACEMENT_3D ( 'NONE', #8504, #15732, #1343 ) ;
#1984=VECTOR ( 'NONE', #1141, 1000.000000000000114 ) ;
#1985=ORIENTED_EDGE ( 'NONE', *, *, #3441, .F. ) ;
#1987=CARTESIAN_POINT ( 'NONE',  ( 89.62416413250210212, 10.32848256004259824, 12.99999999999970157 ) ) ;
#2006=AXIS2_PLACEMENT_3D ( 'NONE', #17289, #15136, #20616 ) ;
#2042=DIRECTION ( 'NONE',  ( -0.9730401042858035643, 0.2306359803922028717, 5.958148513035547083E-17 ) ) ;
#2046=CARTESIAN_POINT ( 'NONE',  ( 42.82341786264429828, 18.59529084842182556, -13.00000000000029665 ) ) ;
#2054=CARTESIAN_POINT ( 'NONE',  ( 34.85451023951635108, 7.825865074983275882, 8.759424124906640685 ) ) ;
#2056=ORIENTED_EDGE ( 'NONE', *, *, #20372, .F. ) ;
#2059=ORIENTED_EDGE ( 'NONE', *, *, #11244, .F. ) ;
#2071=CYLINDRICAL_SURFACE ( 'NONE', #11630, 5.000000000000001776 ) ;
#2088=CARTESIAN_POINT ( 'NONE',  ( 37.61307566641299616, 10.23834044308586044, -8.954072598562484941 ) ) ;
#2131=ORIENTED_EDGE ( 'NONE', *, *, #385, .F. ) ;
#2140=CARTESIAN_POINT ( 'NONE',  ( 35.01760859121469593, 7.342209420739012060, 20.00000000000001066 ) ) ;
#2161=EDGE_CURVE ( 'NONE', #16704, #20682, #13131, .T. ) ;
#2228=DIRECTION ( 'NONE',  ( -0.9730401042858036753, 0.2306359803922028995, 5.958148513035547083E-17 ) ) ;
#2230=EDGE_CURVE ( 'NONE', #6743, #6798, #12017, .T. ) ;
#2259=CARTESIAN_POINT ( 'NONE',  ( 37.46113131852554545, -4.027891576223090020, -13.00000000000000000 ) ) ;
#2270=ORIENTED_EDGE ( 'NONE', *, *, #22306, .T. ) ;
#2287=VERTEX_POINT ( 'NONE', #9368 ) ;
#2307=CONICAL_SURFACE ( 'NONE', #16003, 2.283500000000000529, 0.7853981633974419507 ) ;
#2315=ORIENTED_EDGE ( 'NONE', *, *, #15123, .F. ) ;
#2316=DIRECTION ( 'NONE',  ( -0.9730401042858036753, 0.2306359803922028995, 5.958148513035547083E-17 ) ) ;
#2325=CARTESIAN_POINT ( 'NONE',  ( 37.42777593783879553, 8.782604430957221098, -8.987168322345961968 ) ) ;
#2393=AXIS2_PLACEMENT_3D ( 'NONE', #18291, #20303, #325 ) ;
#2404=CARTESIAN_POINT ( 'NONE',  ( 26.57755037370660034, -6.586732293729930632, 18.00000000000000000 ) ) ;
#2408=CARTESIAN_POINT ( 'NONE',  ( 32.57408586390378247, 18.71231041770077397, -13.00000000000030020 ) ) ;
#2421=CARTESIAN_POINT ( 'NONE',  ( 38.38367524009456844, -0.1357311590789566647, -1.248138659420871028E-15 ) ) ;
#2445=VERTEX_POINT ( 'NONE', #16440 ) ;
#2453=ADVANCED_FACE ( 'NONE', ( #18362 ), #2071, .F. ) ;
#2460=EDGE_LOOP ( 'NONE', ( #23245, #9705 ) ) ;
#2463=FACE_OUTER_BOUND ( 'NONE', #13108, .T. ) ;
#2466=CARTESIAN_POINT ( 'NONE',  ( 35.11747397072455357, 7.763535785894623231, -8.759424124906624698 ) ) ;
#2472=ADVANCED_FACE ( 'NONE', ( #21544 ), #16320, .F. ) ;
#2494=DIRECTION ( 'NONE',  ( -0.2306359803922033158, -0.9730401042858034533, 0.000000000000000000 ) ) ;
#2505=CARTESIAN_POINT ( 'NONE',  ( 30.72899802076640086, 10.92798958341530025, -1.881607274541729715E-15 ) ) ;
#2517=ADVANCED_FACE ( 'NONE', ( #7893 ), #20255, .F. ) ;
#2519=CYLINDRICAL_SURFACE ( 'NONE', #15830, 5.000000000000001776 ) ;
#2550=CARTESIAN_POINT ( 'NONE',  ( 37.46113131852554545, -4.027891576223090020, -13.00000000000000000 ) ) ;
#2569=CARTESIAN_POINT ( 'NONE',  ( 0.000000000000000000, 0.000000000000000000, 0.000000000000000000 ) ) ;
#2616=CYLINDRICAL_SURFACE ( 'NONE', #4170, 5.000000000000001776 ) ;
#2632=VECTOR ( 'NONE', #22694, 1000.000000000000000 ) ;
#2644=CYLINDRICAL_SURFACE ( 'NONE', #11382, 5.000000000000000888 ) ;
#2651=CIRCLE ( 'NONE', #14410, 5.000000000000004441 ) ;
#2657=CARTESIAN_POINT ( 'NONE',  ( 34.88044566782579636, 28.44271146055880095, -18.00000000000029843 ) ) ;
#2661=FACE_OUTER_BOUND ( 'NONE', #11316, .T. ) ;
#2667=CARTESIAN_POINT ( 'NONE',  ( 26.57755037370649731, -6.586732293730120702, -18.00000000000000000 ) ) ;
#2678=EDGE_CURVE ( 'NONE', #6764, #11726, #1747, .T. ) ;
#2770=AXIS2_PLACEMENT_3D ( 'NONE', #15058, #6150, #11183 ) ;
#2773=AXIS2_PLACEMENT_3D ( 'NONE', #572, #7828, #15177 ) ;
#2790=DIRECTION ( 'NONE',  ( 3.356987858687581318E-15, 1.000000000000000000, -5.035481788031372371E-15 ) ) ;
#2810=CARTESIAN_POINT ( 'NONE',  ( 82.99337969622625621, -17.64642043817426043, 13.00000000000000000 ) ) ;
#2818=ORIENTED_EDGE ( 'NONE', *, *, #23140, .F. ) ;
#2873=CARTESIAN_POINT ( 'NONE',  ( 36.17078849317571354, 12.20740994216783193, -20.00000000000001421 ) ) ;
#2883=PLANE ( 'NONE',  #10029 ) ;
#2895=CARTESIAN_POINT ( 'NONE',  ( 37.57450334731217367, 9.167194311959766750, 9.000012392934836569 ) ) ;
#2901=AXIS2_PLACEMENT_3D ( 'NONE', #12, #5608, #14526 ) ;
#2947=VECTOR ( 'NONE', #516, 1000.000000000000114 ) ;
#2957=LINE ( 'NONE', #15317, #10391 ) ;
#2959=EDGE_LOOP ( 'NONE', ( #18310, #3136 ) ) ;
#2964=EDGE_CURVE ( 'NONE', #199, #20542, #15031, .T. ) ;
#2967=CARTESIAN_POINT ( 'NONE',  ( 39.90784330637247024, 24.93874613768021220, -13.00000000000029665 ) ) ;
#2976=AXIS2_PLACEMENT_3D ( 'NONE', #15149, #16828, #8160 ) ;
#2981=DIRECTION ( 'NONE',  ( 0.9730401042858035643, -0.2306359803922028717, -5.958148513035547083E-17 ) ) ;
#3004=CARTESIAN_POINT ( 'NONE',  ( 37.11020026392842652, 8.343731908207489667, 8.942923417076606540 ) ) ;
#3019=CONICAL_SURFACE ( 'NONE', #22331, 2.283500000000000529, 0.7853981633974419507 ) ;
#3041=CARTESIAN_POINT ( 'NONE',  ( 33.65824643301471042, 10.51177500877083659, -8.996924156394149108 ) ) ;
#3061=CARTESIAN_POINT ( 'NONE',  ( 26.11627841292215280, -8.532812502301741375, -20.00000000000000000 ) ) ;
#3072=CONICAL_SURFACE ( 'NONE', #16340, 2.283500000000000529, 0.7853981633974539411 ) ;
#3128=CARTESIAN_POINT ( 'NONE',  ( 36.05798491156198082, 7.755984563572242863, 8.806404184311324101 ) ) ;
#3136=ORIENTED_EDGE ( 'NONE', *, *, #8962, .F. ) ;
#3169=CARTESIAN_POINT ( 'NONE',  ( 33.53333525001635707, 9.983743838774772783, -8.996869837679783544 ) ) ;
#3198=FACE_BOUND ( 'NONE', #22784, .T. ) ;
#3210=( LENGTH_UNIT ( ) NAMED_UNIT ( * ) SI_UNIT ( .MILLI., .METRE. ) );
#3234=DIRECTION ( 'NONE',  ( 6.123230159571619958E-17, 0.000000000000000000, 1.000000000000000000 ) ) ;
#3242=CARTESIAN_POINT ( 'NONE',  ( 36.33223090203711791, 11.71027499018234153, 8.762640180330951267 ) ) ;
#3252=DIRECTION ( 'NONE',  ( -1.227507208848341976E-15, -4.920447605136010024E-15, -1.000000000000000000 ) ) ;
#3272=VERTEX_POINT ( 'NONE', #3888 ) ;
#3274=AXIS2_PLACEMENT_3D ( 'NONE', #10119, #7976, #22447 ) ;
#3277=CARTESIAN_POINT ( 'NONE',  ( 34.17078830033462822, 8.269992485274588745, -8.820012287919192673 ) ) ;
#3318=B_SPLINE_CURVE_WITH_KNOTS ( 'NONE', 3,
 ( #19517, #10049, #12176, #1332, #19400, #3128, #6451, #20823, #14051, #15836, #3004, #19175, #6817, #21293, #2895, #15480, #8712, #10161, #5032, #13827, #23177, #17393, #23063, #12297, #1215, #1094, #8358, #3242, #15944, #12060 ),
 .UNSPECIFIED., .F., .F.,
 ( 4, 2, 2, 2, 2, 2, 2, 2, 2, 2, 2, 2, 2, 2, 4 ),
 ( 0.006516123109207543583, 0.006923489735540620284, 0.007330856361873697852, 0.007738222988206774552, 0.008145589614539851253, 0.008960322867206008124, 0.009367689493539088294, 0.009775056119872168464, 0.01018242274620524863, 0.01058978937253832880, 0.01140452262520448741, 0.01181188925153756064, 0.01221925587787063561, 0.01262662250420371057, 0.01303398913053678380 ),
 .UNSPECIFIED. ) ;
#3350=CIRCLE ( 'NONE', #9429, 2.750000000000002220 ) ;
#3364=EDGE_LOOP ( 'NONE', ( #18040, #9753 ) ) ;
#3365=DIRECTION ( 'NONE',  ( 0.2306359803922033713, 0.9730401042858034533, -4.558064749665356219E-15 ) ) ;
#3378=CYLINDRICAL_SURFACE ( 'NONE', #17986, 9.000000000000001776 ) ;
#3379=EDGE_LOOP ( 'NONE', ( #16641, #2056, #22053, #23314 ) ) ;
#3383=EDGE_CURVE ( 'NONE', #4635, #20542, #22723, .T. ) ;
#3409=LINE ( 'NONE', #4880, #23448 ) ;
#3420=ORIENTED_EDGE ( 'NONE', *, *, #18127, .T. ) ;
#3422=VERTEX_POINT ( 'NONE', #5793 ) ;
#3423=ADVANCED_FACE ( 'NONE', ( #14585 ), #3072, .F. ) ;
#3424=AXIS2_PLACEMENT_3D ( 'NONE', #14001, #22550, #6294 ) ;
#3427=ORIENTED_EDGE ( 'NONE', *, *, #10719, .T. ) ;
#3434=AXIS2_PLACEMENT_3D ( 'NONE', #2259, #2, #14738 ) ;
#3441=EDGE_CURVE ( 'NONE', #17345, #11267, #6881, .T. ) ;
#3453=DIRECTION ( 'NONE',  ( 0.9730401042858035643, -0.2306359803922028717, -5.958148513035547083E-17 ) ) ;
#3481=EDGE_LOOP ( 'NONE', ( #9777, #10910, #16130, #13421 ) ) ;
#3486=ORIENTED_EDGE ( 'NONE', *, *, #20683, .T. ) ;
#3493=DIRECTION ( 'NONE',  ( -0.9730401042858036753, 0.2306359803922028995, 5.958148513035547083E-17 ) ) ;
#3497=VECTOR ( 'NONE', #21930, 1000.000000000000000 ) ;
#3513=FACE_BOUND ( 'NONE', #10665, .T. ) ;
#3516=AXIS2_PLACEMENT_3D ( 'NONE', #2667, #17160, #19069 ) ;
#3568=CYLINDRICAL_SURFACE ( 'NONE', #2393, 2.750000000000000000 ) ;
#3579=FACE_OUTER_BOUND ( 'NONE', #5128, .T. ) ;
#3605=CARTESIAN_POINT ( 'NONE',  ( 34.39395800938287096, 11.46298095551878227, 8.896276805998372339 ) ) ;
#3667=AXIS2_PLACEMENT_3D ( 'NONE', #15140, #20270, #16564 ) ;
#3670=LINE ( 'NONE', #1880, #5426 ) ;
#3672=ORIENTED_EDGE ( 'NONE', *, *, #21381, .T. ) ;
#3682=ORIENTED_EDGE ( 'NONE', *, *, #20388, .T. ) ;
#3683=DIRECTION ( 'NONE',  ( -0.2306359803922031770, -0.9730401042858034533, 0.000000000000000000 ) ) ;
#3695=DIRECTION ( 'NONE',  ( -0.2306359803922033158, -0.9730401042858034533, 0.000000000000000000 ) ) ;
#3780=PRODUCT_DEFINITION_FORMATION_WITH_SPECIFIED_SOURCE ( 'ANY', '', #5117, .NOT_KNOWN. ) ;
#3781=VERTEX_POINT ( 'NONE', #14782 ) ;
#3782=AXIS2_PLACEMENT_3D ( 'NONE', #814, #12014, #8558 ) ;
#3787=FACE_BOUND ( 'NONE', #16674, .T. ) ;
#3810=CARTESIAN_POINT ( 'NONE',  ( 33.27705887009660302, -3.036156860536619817, -13.00000000000000000 ) ) ;
#3833=AXIS2_PLACEMENT_3D ( 'NONE', #876, #6108, #22137 ) ;
#3837=CARTESIAN_POINT ( 'NONE',  ( 42.82341786264430539, 18.59529084842194280, 12.99999999999970512 ) ) ;
#3838=ADVANCED_FACE ( 'NONE', ( #5525 ), #2307, .F. ) ;
#3841=DIRECTION ( 'NONE',  ( -0.9730401042858036753, 0.2306359803922028995, 5.958148513035547083E-17 ) ) ;
#3843=CARTESIAN_POINT ( 'NONE',  ( 40.42677426225490933, 27.12808637232345177, 12.99999999999979927 ) ) ;
#3855=FACE_OUTER_BOUND ( 'NONE', #6242, .T. ) ;
#3884=VECTOR ( 'NONE', #10062, 1000.000000000000000 ) ;
#3888=CARTESIAN_POINT ( 'NONE',  ( 38.09538026460416660, -1.352031289437040318, 13.00000000000000355 ) ) ;
#3928=DIRECTION ( 'NONE',  ( -0.9730401042858035643, 0.2306359803922028717, 5.958148513035547083E-17 ) ) ;
#3932=ORIENTED_EDGE ( 'NONE', *, *, #22306, .F. ) ;
#3984=EDGE_LOOP ( 'NONE', ( #10242, #4174 ) ) ;
#3997=PLANE ( 'NONE',  #21918 ) ;
#4007=DIRECTION ( 'NONE',  ( 0.2306359803922033713, 0.9730401042858034533, -4.558064749665356219E-15 ) ) ;
#4035=CARTESIAN_POINT ( 'NONE',  ( 43.45766680872284837, 21.27115113520789791, 12.99999999999970157 ) ) ;
#4057=ORIENTED_EDGE ( 'NONE', *, *, #8962, .T. ) ;
#4092=DIRECTION ( 'NONE',  ( -0.9730401042858035643, 0.2306359803922028717, 5.958148513035547083E-17 ) ) ;
#4105=ORIENTED_EDGE ( 'NONE', *, *, #8140, .F. ) ;
#4170=AXIS2_PLACEMENT_3D ( 'NONE', #13432, #3928, #16860 ) ;
#4174=ORIENTED_EDGE ( 'NONE', *, *, #12693, .T. ) ;
#4219=CARTESIAN_POINT ( 'NONE',  ( 35.34725016111838869, 18.05499787358318287, 12.99999999999979927 ) ) ;
#4228=FACE_OUTER_BOUND ( 'NONE', #21178, .T. ) ;
#4239=CARTESIAN_POINT ( 'NONE',  ( 37.65360996504041680, 27.78539891644121695, 12.99999999999979927 ) ) ;
#4240=AXIS2_PLACEMENT_3D ( 'NONE', #21065, #20945, #2790 ) ;
#4282=DIRECTION ( 'NONE',  ( -0.9730401042858035643, 0.2306359803922028717, 5.958148513035547083E-17 ) ) ;
#4289=ORIENTED_EDGE ( 'NONE', *, *, #19831, .T. ) ;
#4290=VECTOR ( 'NONE', #11233, 999.9999999999998863 ) ;
#4310=DIRECTION ( 'NONE',  ( -0.2306359803922026497, -0.9730401042858035643, 0.000000000000000000 ) ) ;
#4343=DIRECTION ( 'NONE',  ( -0.2306359803922033436, -0.9730401042858034533, 0.000000000000000000 ) ) ;
#4355=CARTESIAN_POINT ( 'NONE',  ( 37.63679421689584359, 9.430002510136448635, -9.000012045631684998 ) ) ;
#4375=CARTESIAN_POINT ( 'NONE',  ( 36.76922337734900026, -6.947011889080330960, 20.00000000000000000 ) ) ;
#4400=AXIS2_PLACEMENT_3D ( 'NONE', #12927, #7370, #12708 ) ;
#4421=EDGE_CURVE ( 'NONE', #3781, #20776, #14611, .T. ) ;
#4503=FACE_OUTER_BOUND ( 'NONE', #22318, .T. ) ;
#4512=ORIENTED_EDGE ( 'NONE', *, *, #23140, .T. ) ;
#4563=LINE ( 'NONE', #17286, #21332 ) ;
#4600=VERTEX_POINT ( 'NONE', #8695 ) ;
#4624=ORIENTED_EDGE ( 'NONE', *, *, #21314, .T. ) ;
#4635=VERTEX_POINT ( 'NONE', #10030 ) ;
#4733=VERTEX_POINT ( 'NONE', #1193 ) ;
#4764=VERTEX_POINT ( 'NONE', #1545 ) ;
#4780=CARTESIAN_POINT ( 'NONE',  ( 35.59419854219520118, 9.774809681453518806, 19.78350000000000009 ) ) ;
#4789=DIRECTION ( 'NONE',  ( -0.2306359803922031770, -0.9730401042858034533, 0.000000000000000000 ) ) ;
#4811=EDGE_CURVE ( 'NONE', #22224, #1981, #14781, .T. ) ;
#4831=CIRCLE ( 'NONE', #14690, 5.000000000000000888 ) ;
#4838=CIRCLE ( 'NONE', #15440, 9.000000000000005329 ) ;
#4840=EDGE_CURVE ( 'NONE', #4733, #12382, #2651, .T. ) ;
#4856=DIRECTION ( 'NONE',  ( 6.123230159571619958E-17, 0.000000000000000000, 1.000000000000000000 ) ) ;
#4880=CARTESIAN_POINT ( 'NONE',  ( 34.88044566782584610, 28.44271146055880095, -18.00000000000029843 ) ) ;
#4882=PRODUCT_DEFINITION ( 'UNKNOWN', '', #3780, #15632 ) ;
#4900=CARTESIAN_POINT ( 'NONE',  ( 36.76922337734895052, -6.947011889080550340, -20.00000000000000000 ) ) ;
#4918=VERTEX_POINT ( 'NONE', #7965 ) ;
#4932=ADVANCED_FACE ( 'NONE', ( #22079 ), #2616, .F. ) ;
#4945=CARTESIAN_POINT ( 'NONE',  ( 33.61438040303559660, 10.38400890524524023, -8.999987531128509133 ) ) ;
#4951=VECTOR ( 'NONE', #21621, 999.9999999999998863 ) ;
#4986=CARTESIAN_POINT ( 'NONE',  ( 35.34171762861019772, 30.38879166913045182, -16.00000000000029843 ) ) ;
#5032=CARTESIAN_POINT ( 'NONE',  ( 37.65606570105540385, 9.973062512861897488, 8.976009386856667049 ) ) ;
#5033=CYLINDRICAL_SURFACE ( 'NONE', #22240, 2.750000000000000888 ) ;
#5050=EDGE_CURVE ( 'NONE', #20682, #16704, #731, .T. ) ;
#5113=EDGE_CURVE ( 'NONE', #3781, #4635, #11778, .T. ) ;
#5117=PRODUCT ( '1602p_c_36', '1602p_c_36', '', ( #23378 ) ) ;
#5128=EDGE_LOOP ( 'NONE', ( #18873, #5468, #7997, #11045, #9308, #2818, #22170, #22633 ) ) ;
#5134=DIRECTION ( 'NONE',  ( -0.9730401042858036753, 0.2306359803922028995, 5.958148513035547083E-17 ) ) ;
#5147=CARTESIAN_POINT ( 'NONE',  ( 36.50043006307940630, 22.92019839501199741, -13.00000000000030020 ) ) ;
#5164=CARTESIAN_POINT ( 'NONE',  ( 35.59419854219520118, 9.774809681453239918, -37.44562646538079775 ) ) ;
#5170=DIRECTION ( 'NONE',  ( -0.2306359803922031215, -0.9730401042858033422, 0.000000000000000000 ) ) ;
#5213=ORIENTED_EDGE ( 'NONE', *, *, #10290, .F. ) ;
#5232=VECTOR ( 'NONE', #16909, 999.9999999999998863 ) ;
#5261=EDGE_CURVE ( 'NONE', #8547, #11347, #14042, .T. ) ;
#5273=EDGE_CURVE ( 'NONE', #20204, #9841, #10233, .T. ) ;
#5300=EDGE_CURVE ( 'NONE', #20016, #21792, #9219, .T. ) ;
#5312=CYLINDRICAL_SURFACE ( 'NONE', #16169, 5.000000000000000888 ) ;
#5325=ORIENTED_EDGE ( 'NONE', *, *, #1097, .T. ) ;
#5361=CARTESIAN_POINT ( 'NONE',  ( 26.11627841292220253, -8.532812502301570845, 16.00000000000000000 ) ) ;
#5378=ORIENTED_EDGE ( 'NONE', *, *, #23018, .T. ) ;
#5380=CARTESIAN_POINT ( 'NONE',  ( 34.99546711040250102, 11.77144200483400915, 8.817835639223813970 ) ) ;
#5382=ORIENTED_EDGE ( 'NONE', *, *, #517, .T. ) ;
#5405=DIRECTION ( 'NONE',  ( -0.9730401042858035643, 0.2306359803922028717, 5.958148513035547083E-17 ) ) ;
#5426=VECTOR ( 'NONE', #7588, 999.9999999999998863 ) ;
#5462=VECTOR ( 'NONE', #17829, 1000.000000000000114 ) ;
#5468=ORIENTED_EDGE ( 'NONE', *, *, #5300, .F. ) ;
#5485=DIRECTION ( 'NONE',  ( -0.9730401042858035643, 0.2306359803922028717, 5.958148513035547083E-17 ) ) ;
#5489=EDGE_LOOP ( 'NONE', ( #8438, #20778, #11834, #1227 ) ) ;
#5503=CARTESIAN_POINT ( 'NONE',  ( 33.57591379187338987, 9.308427061869513963, 8.953813951970682083 ) ) ;
#5525=FACE_OUTER_BOUND ( 'NONE', #21960, .T. ) ;
#5535=LINE ( 'NONE', #12561, #20401 ) ;
#5580=CARTESIAN_POINT ( 'NONE',  ( 33.72726576586484981, 23.57751093913000062, 12.99999999999979927 ) ) ;
#5598=EDGE_CURVE ( 'NONE', #18732, #12382, #11370, .T. ) ;
#5606=CARTESIAN_POINT ( 'NONE',  ( 45.07211867146820339, 28.08243186520840240, -16.00000000000029843 ) ) ;
#5608=DIRECTION ( 'NONE',  ( 5.899155740360660338E-30, 4.861311874477930828E-15, 1.000000000000000000 ) ) ;
#5612=CARTESIAN_POINT ( 'NONE',  ( 33.51993406171253298, 9.985323737508171149, 8.999975802806215341 ) ) ;
#5621=CARTESIAN_POINT ( 'NONE',  ( 26.11627841292220253, -8.532812502301538871, 20.00000000000000000 ) ) ;
#5622=AXIS2_PLACEMENT_3D ( 'NONE', #11710, #9914, #8596 ) ;
#5649=CARTESIAN_POINT ( 'NONE',  ( 35.11747397072455357, 7.763535785894623231, -8.759424124906624698 ) ) ;
#5652=ORIENTED_EDGE ( 'NONE', *, *, #19429, .F. ) ;
#5738=FACE_BOUND ( 'NONE', #2959, .T. ) ;
#5750=FACE_BOUND ( 'NONE', #19351, .T. ) ;
#5751=DIRECTION ( 'NONE',  ( -0.9744196363770861735, -1.527762929736005432E-17, -0.2247362281492400471 ) ) ;
#5793=CARTESIAN_POINT ( 'NONE',  ( 27.03882233449100170, -4.640652085158319728, 20.00000000000000000 ) ) ;
#5800=CARTESIAN_POINT ( 'NONE',  ( 35.11747397072451804, 7.763535785894483787, -37.44562646538079065 ) ) ;
#5824=LINE ( 'NONE', #7720, #12598 ) ;
#5832=EDGE_LOOP ( 'NONE', ( #11228, #8524 ) ) ;
#5850=CARTESIAN_POINT ( 'NONE',  ( 30.50389457288209982, -2.378844316418729843, 13.00000000000000000 ) ) ;
#5878=DIRECTION ( 'NONE',  ( -0.9730401042858035643, 0.2306359803922028717, 5.958148513035547083E-17 ) ) ;
#5881=ORIENTED_EDGE ( 'NONE', *, *, #15746, .F. ) ;
#5892=CARTESIAN_POINT ( 'NONE',  ( 37.65622438626208890, 9.971723439402808253, -8.976109897029356688 ) ) ;
#5909=CARTESIAN_POINT ( 'NONE',  ( 36.12085580342079538, 11.99674675959015246, 19.78349999999998943 ) ) ;
#5957=CYLINDRICAL_SURFACE ( 'NONE', #6854, 2.750000000000000888 ) ;
#5961=DIRECTION ( 'NONE',  ( -0.2306359803922026497, -0.9730401042858035643, 0.000000000000000000 ) ) ;
#5969=DIRECTION ( 'NONE',  ( -0.9730401042858036753, 0.2306359803922028995, 5.958148513035547083E-17 ) ) ;
#6012=ORIENTED_EDGE ( 'NONE', *, *, #4421, .F. ) ;
#6054=DIRECTION ( 'NONE',  ( -0.2306359803922033991, -0.9730401042858033422, 0.000000000000000000 ) ) ;
#6097=CARTESIAN_POINT ( 'NONE',  ( 83.62762864230479920, -14.97056015138839946, -13.00000000000000000 ) ) ;
#6107=CARTESIAN_POINT ( 'NONE',  ( 83.62762864230479920, -14.97056015138829821, 13.00000000000000000 ) ) ;
#6108=DIRECTION ( 'NONE',  ( 0.9730401042858035643, -0.2306359803922028717, -5.958148513035547083E-17 ) ) ;
#6117=ORIENTED_EDGE ( 'NONE', *, *, #3383, .F. ) ;
#6118=CARTESIAN_POINT ( 'NONE',  ( 39.27359436029389883, 22.26288585089439920, 12.99999999999970157 ) ) ;
#6124=CIRCLE ( 'NONE', #427, 2.750000000000002220 ) ;
#6150=DIRECTION ( 'NONE',  ( -0.9730401042858035643, 0.2306359803922028717, 5.958148513035547083E-17 ) ) ;
#6163=ADVANCED_FACE ( 'NONE', ( #18922 ), #2644, .F. ) ;
#6176=DIRECTION ( 'NONE',  ( 6.123230159571619958E-17, 0.000000000000000000, 1.000000000000000000 ) ) ;
#6181=VERTEX_POINT ( 'NONE', #2421 ) ;
#6186=ORIENTED_EDGE ( 'NONE', *, *, #7899, .T. ) ;
#6225=ADVANCED_FACE ( 'NONE', ( #19505 ), #3019, .F. ) ;
#6230=EDGE_CURVE ( 'NONE', #645, #8547, #10496, .T. ) ;
#6242=EDGE_LOOP ( 'NONE', ( #5652, #6186, #18069, #8899 ) ) ;
#6243=PLANE ( 'NONE',  #3516 ) ;
#6246=DIRECTION ( 'NONE',  ( -0.9730401042858035643, 0.2306359803922028717, 5.958148513035547083E-17 ) ) ;
#6255=DIRECTION ( 'NONE',  ( 0.1630842657209352065, 0.6880432561069602659, 0.7071067811865442421 ) ) ;
#6288=ADVANCED_FACE ( 'NONE', ( #12283 ), #8229, .T. ) ;
#6291=DIRECTION ( 'NONE',  ( -0.9730401042858036753, 0.2306359803922028995, 5.958148513035547083E-17 ) ) ;
#6294=DIRECTION ( 'NONE',  ( -0.2306359803922032603, -0.9730401042858034533, 0.000000000000000000 ) ) ;
#6314=ADVANCED_FACE ( 'NONE', ( #1437, #8702 ), #2883, .T. ) ;
#6315=DIRECTION ( 'NONE',  ( -0.9730401042858035643, 0.2306359803922028717, 5.958148513035547083E-17 ) ) ;
#6324=LINE ( 'NONE', #17010, #19846 ) ;
#6367=CARTESIAN_POINT ( 'NONE',  ( 43.45766680872284837, 21.27115113520779843, -13.00000000000030020 ) ) ;
#6392=AXIS2_PLACEMENT_3D ( 'NONE', #14274, #12397, #23409 ) ;
#6451=CARTESIAN_POINT ( 'NONE',  ( 36.19076168202141019, 7.791205907825823118, 8.820012287919203331 ) ) ;
#6452=DIRECTION ( 'NONE',  ( -0.2306359803922009288, -0.9730401042858040084, 0.000000000000000000 ) ) ;
#6466=ORIENTED_EDGE ( 'NONE', *, *, #13044, .F. ) ;
#6485=ORIENTED_EDGE ( 'NONE', *, *, #249, .F. ) ;
#6489=EDGE_CURVE ( 'NONE', #1396, #2445, #11105, .T. ) ;
#6546=VECTOR ( 'NONE', #15553, 999.9999999999998863 ) ;
#6591=CARTESIAN_POINT ( 'NONE',  ( 27.73073027566755044, -1.721531772301079899, -13.00000000000000000 ) ) ;
#6626=CARTESIAN_POINT ( 'NONE',  ( 33.53206126189282088, 9.578550183514808580, -8.976164948525093834 ) ) ;
#6666=CARTESIAN_POINT ( 'NONE',  ( 26.57755037370653639, -6.586732293730098498, -13.00000000000000000 ) ) ;
#6719=CARTESIAN_POINT ( 'NONE',  ( 36.17078849317570644, 12.20740994216802910, 19.99999999999998934 ) ) ;
#6741=EDGE_CURVE ( 'NONE', #20016, #9507, #10352, .T. ) ;
#6743=VERTEX_POINT ( 'NONE', #1409 ) ;
#6764=VERTEX_POINT ( 'NONE', #6666 ) ;
#6775=ORIENTED_EDGE ( 'NONE', *, *, #11244, .T. ) ;
#6798=VERTEX_POINT ( 'NONE', #2967 ) ;
#6804=DIRECTION ( 'NONE',  ( 1.213490492418603984E-15, 4.861311874477930828E-15, 1.000000000000000000 ) ) ;
#6808=CARTESIAN_POINT ( 'NONE',  ( 38.63934541421534163, 19.58702556410841922, 12.99999999999970512 ) ) ;
#6817=CARTESIAN_POINT ( 'NONE',  ( 37.41678276236235234, 8.790432847337626754, 8.984918777770046106 ) ) ;
#6832=ORIENTED_EDGE ( 'NONE', *, *, #3441, .T. ) ;
#6854=AXIS2_PLACEMENT_3D ( 'NONE', #7984, #11575, #9888 ) ;
#6871=AXIS2_PLACEMENT_3D ( 'NONE', #22162, #17950, #19600 ) ;
#6880=ORIENTED_EDGE ( 'NONE', *, *, #1144, .F. ) ;
#6881=CIRCLE ( 'NONE', #15971, 5.000000000000002665 ) ;
#6925=CARTESIAN_POINT ( 'NONE',  ( 33.27705887009660302, -3.036156860536640245, -13.00000000000000000 ) ) ;
#6946=CYLINDRICAL_SURFACE ( 'NONE', #14677, 5.000000000000001776 ) ;
#6976=CARTESIAN_POINT ( 'NONE',  ( 36.07092311366589854, 11.78608357701213905, -8.759424124907058129 ) ) ;
#6987=CARTESIAN_POINT ( 'NONE',  ( 34.07732981382596193, 11.20451025314141624, -8.943038809424274760 ) ) ;
#6996=VECTOR ( 'NONE', #14080, 999.9999999999998863 ) ;
#7036=CARTESIAN_POINT ( 'NONE',  ( 44.61084671068389440, 26.13635165663700022, 17.99999999999970157 ) ) ;
#7040=ORIENTED_EDGE ( 'NONE', *, *, #5273, .F. ) ;
#7052=LINE ( 'NONE', #14041, #20489 ) ;
#7074=ORIENTED_EDGE ( 'NONE', *, *, #19989, .T. ) ;
#7082=DIRECTION ( 'NONE',  ( 0.2306359803922017615, 0.9730401042858037863, -3.356987858687580135E-15 ) ) ;
#7094=ADVANCED_FACE ( 'NONE', ( #16845, #11399, #18638, #317, #20177, #22409 ), #7820, .F. ) ;
#7121=EDGE_CURVE ( 'NONE', #17345, #6764, #11293, .T. ) ;
#7122=FACE_OUTER_BOUND ( 'NONE', #3984, .T. ) ;
#7151=ORIENTED_EDGE ( 'NONE', *, *, #12692, .T. ) ;
#7157=CARTESIAN_POINT ( 'NONE',  ( 35.84667945578014780, -10.83917230622373928, -16.00000000000000000 ) ) ;
#7163=LINE ( 'NONE', #14389, #4951 ) ;
#7176=CARTESIAN_POINT ( 'NONE',  ( 35.93758199568961942, 11.81768891304677815, 8.759424124907043918 ) ) ;
#7187=LINE ( 'NONE', #10886, #15450 ) ;
#7197=DIRECTION ( 'NONE',  ( -0.9730401042858035643, 0.2306359803922028717, 5.958148513035547083E-17 ) ) ;
#7211=EDGE_LOOP ( 'NONE', ( #1806, #5382, #10169, #10983 ) ) ;
#7223=CARTESIAN_POINT ( 'NONE',  ( 35.01760859121468883, 7.342209420738806891, -19.99999999999998579 ) ) ;
#7292=CARTESIAN_POINT ( 'NONE',  ( 33.83992520232241930, 10.87628626253941277, 8.976109897029353135 ) ) ;
#7330=EDGE_CURVE ( 'NONE', #2287, #16704, #19085, .T. ) ;
#7347=EDGE_CURVE ( 'NONE', #13560, #9664, #21357, .T. ) ;
#7366=ORIENTED_EDGE ( 'NONE', *, *, #6741, .F. ) ;
#7370=DIRECTION ( 'NONE',  ( -0.9730401042858035643, 0.2306359803922028717, 5.958148513035547083E-17 ) ) ;
#7383=FACE_BOUND ( 'NONE', #23335, .T. ) ;
#7404=CARTESIAN_POINT ( 'NONE',  ( 26.11627841292215280, -8.532812502301570845, 16.00000000000000000 ) ) ;
#7414=ORIENTED_EDGE ( 'NONE', *, *, #12692, .F. ) ;
#7437=CARTESIAN_POINT ( 'NONE',  ( 38.12041445833288122, 17.39768532946541413, 12.99999999999979927 ) ) ;
#7444=CARTESIAN_POINT ( 'NONE',  ( 36.05743075878378789, 7.755885733951535244, -8.806355889830928874 ) ) ;
#7457=DIRECTION ( 'NONE',  ( -0.2306359803922010121, -0.9730401042858040084, 0.000000000000000000 ) ) ;
#7481=EDGE_CURVE ( 'NONE', #16195, #199, #13120, .T. ) ;
#7485=DIRECTION ( 'NONE',  ( -1.226293361205523864E-15, -4.915326450861021157E-15, -1.000000000000000000 ) ) ;
#7504=ADVANCED_FACE ( 'NONE', ( #22353 ), #21031, .F. ) ;
#7524=CARTESIAN_POINT ( 'NONE',  ( 33.61414435712650572, 10.38347584602063911, 9.000012045631683222 ) ) ;
#7531=CARTESIAN_POINT ( 'NONE',  ( 88.98991518642344545, 7.652622273256539209, -13.00000000000030020 ) ) ;
#7553=DIRECTION ( 'NONE',  ( 1.226293361205523864E-15, 4.915326450861021157E-15, 1.000000000000000000 ) ) ;
#7554=VERTEX_POINT ( 'NONE', #8321 ) ;
#7588=DIRECTION ( 'NONE',  ( -0.2306359803922028995, -0.9730401042858036753, 5.121148285185918258E-15 ) ) ;
#7606=EDGE_LOOP ( 'NONE', ( #14646, #4624 ) ) ;
#7644=DIRECTION ( 'NONE',  ( 1.000000000000000000, -1.213490492418610097E-15, 0.000000000000000000 ) ) ;
#7654=LINE ( 'NONE', #17024, #5232 ) ;
#7666=CIRCLE ( 'NONE', #4240, 2.066999999999999282 ) ;
#7674=CARTESIAN_POINT ( 'NONE',  ( 36.69831606175046090, 11.52739241660666814, -8.784148981162500647 ) ) ;
#7689=DIRECTION ( 'NONE',  ( -0.9730401042858035643, 0.2306359803922028717, 5.958148513035547083E-17 ) ) ;
#7714=AXIS2_PLACEMENT_3D ( 'NONE', #6097, #22798, #18586 ) ;
#7720=CARTESIAN_POINT ( 'NONE',  ( 45.07211867146829576, 28.08243186520860135, 19.99999999999969802 ) ) ;
#7750=EDGE_CURVE ( 'NONE', #142, #3422, #1181, .T. ) ;
#7769=DIRECTION ( 'NONE',  ( -0.1630842657209323754, -0.6880432561069493858, 0.7071067811865554553 ) ) ;
#7794=CARTESIAN_POINT ( 'NONE',  ( 37.54227681792503546, 9.031923193207390455, -8.999975802806220671 ) ) ;
#7820=PLANE ( 'NONE',  #2770 ) ;
#7822=VECTOR ( 'NONE', #8320, 999.9999999999998863 ) ;
#7823=ADVANCED_FACE ( 'NONE', ( #10944 ), #3568, .F. ) ;
#7825=DIRECTION ( 'NONE',  ( -0.2306359803922027607, -0.9730401042858035643, 0.000000000000000000 ) ) ;
#7828=DIRECTION ( 'NONE',  ( -1.213490492418603984E-15, -4.861311874477930828E-15, -1.000000000000000000 ) ) ;
#7838=DIRECTION ( 'NONE',  ( -0.2306359803922026497, -0.9730401042858035643, 0.000000000000000000 ) ) ;
#7860=AXIS2_PLACEMENT_3D ( 'NONE', #5147, #17506, #1098 ) ;
#7893=FACE_OUTER_BOUND ( 'NONE', #3379, .T. ) ;
#7899=EDGE_CURVE ( 'NONE', #22544, #21046, #3670, .T. ) ;
#7910=PLANE ( 'NONE',  #3667 ) ;
#7923=ORIENTED_EDGE ( 'NONE', *, *, #5113, .F. ) ;
#7960=DIRECTION ( 'NONE',  ( -0.9730401042858035643, 0.2306359803922028717, 5.958148513035547083E-17 ) ) ;
#7965=CARTESIAN_POINT ( 'NONE',  ( 39.90784330637245603, 24.93874613768034010, 12.99999999999970512 ) ) ;
#7976=DIRECTION ( 'NONE',  ( 1.213490492418610097E-15, 4.861311874477940294E-15, 1.000000000000000000 ) ) ;
#7984=CARTESIAN_POINT ( 'NONE',  ( 83.62762864230479920, -14.97056015138829821, 13.00000000000000000 ) ) ;
#7988=FACE_OUTER_BOUND ( 'NONE', #16969, .T. ) ;
#7991=ORIENTED_EDGE ( 'NONE', *, *, #23206, .T. ) ;
#7997=ORIENTED_EDGE ( 'NONE', *, *, #13062, .F. ) ;
#8017=DIRECTION ( 'NONE',  ( -0.9730401042858035643, 0.2306359803922028717, 5.958148513035547083E-17 ) ) ;
#8022=EDGE_LOOP ( 'NONE', ( #8263, #8434, #18506, #16046 ) ) ;
#8040=DIRECTION ( 'NONE',  ( 0.000000000000000000, 1.000000000000000000, -5.551115123125781913E-15 ) ) ;
#8044=CARTESIAN_POINT ( 'NONE',  ( 34.60900853987882897, 7.952645293563162632, -8.774947752588866834 ) ) ;
#8094=CIRCLE ( 'NONE', #15279, 2.750000000000002220 ) ;
#8140=EDGE_CURVE ( 'NONE', #16195, #4635, #101, .T. ) ;
#8142=DIRECTION ( 'NONE',  ( -0.9730401042858035643, 0.2306359803922028717, 5.958148513035547083E-17 ) ) ;
#8158=DIRECTION ( 'NONE',  ( 0.9730401042858036753, -0.2306359803922028995, -5.958148513035547083E-17 ) ) ;
#8160=DIRECTION ( 'NONE',  ( -0.2306359803922033436, -0.9730401042858034533, 0.000000000000000000 ) ) ;
#8229=PLANE ( 'NONE',  #21377 ) ;
#8236=CARTESIAN_POINT ( 'NONE',  ( 33.91130781617516732, -0.3602965737506598209, -12.99999999999999645 ) ) ;
#8243=CARTESIAN_POINT ( 'NONE',  ( 39.27359436029389883, 22.26288585089424998, -13.00000000000030020 ) ) ;
#8263=ORIENTED_EDGE ( 'NONE', *, *, #1412, .T. ) ;
#8272=AXIS2_PLACEMENT_3D ( 'NONE', #17676, #11877, #11993 ) ;
#8283=CARTESIAN_POINT ( 'NONE',  ( 34.49266682421115604, 8.020563254273458398, -8.783920975641599682 ) ) ;
#8296=CARTESIAN_POINT ( 'NONE',  ( 88.98991518642354492, 7.652622273256637797, 12.99999999999970157 ) ) ;
#8307=CARTESIAN_POINT ( 'NONE',  ( 44.09191575480141978, 23.94701142199374289, -13.00000000000029665 ) ) ;
#8311=CARTESIAN_POINT ( 'NONE',  ( 36.07092311366587722, 11.78608357701199694, -37.44562646538080486 ) ) ;
#8317=B_SPLINE_CURVE_WITH_KNOTS ( 'NONE', 3,
 ( #9228, #12900, #11376, #18490, #7674, #13378, #9713, #14919, #16926, #22151, #2088, #5892, #13141, #18610, #4355, #7794, #2325, #9588, #22261, #16818, #18252, #1968, #16458, #176, #7444, #21915, #11150, #5649 ),
 .UNSPECIFIED., .F., .F.,
 ( 4, 2, 2, 2, 2, 2, 2, 2, 2, 2, 2, 2, 2, 4 ),
 ( 0.000000000000000000, 0.0004072576943254699561, 0.0008145153886509399121, 0.001629030777301882426, 0.002036288471627355906, 0.002443546165952829169, 0.002850803860278303299, 0.003258061554603776128, 0.004072576943254728292, 0.004479834637580206759, 0.004887092331905683491, 0.005294350026231164560, 0.005701607720556645630, 0.006516123109207627717 ),
 .UNSPECIFIED. ) ;
#8320=DIRECTION ( 'NONE',  ( 0.9730401042858036753, -0.2306359803922028995, -5.958148513035547083E-17 ) ) ;
#8321=CARTESIAN_POINT ( 'NONE',  ( 35.11747397072455357, 7.763535785894623231, -8.759424124906624698 ) ) ;
#8358=CARTESIAN_POINT ( 'NONE',  ( 36.57773002789497241, 11.59782464082818798, 8.774845639077975434 ) ) ;
#8397=CARTESIAN_POINT ( 'NONE',  ( 33.98781586735240268, 8.467099387652083919, -8.849098278953663410 ) ) ;
#8434=ORIENTED_EDGE ( 'NONE', *, *, #6230, .T. ) ;
#8438=ORIENTED_EDGE ( 'NONE', *, *, #8768, .T. ) ;
#8457=ORIENTED_EDGE ( 'NONE', *, *, #6489, .F. ) ;
#8479=LINE ( 'NONE', #22943, #22765 ) ;
#8504=CARTESIAN_POINT ( 'NONE',  ( 35.59419854219520118, 9.774809681453239918, -37.44562646538079775 ) ) ;
#8524=ORIENTED_EDGE ( 'NONE', *, *, #10576, .T. ) ;
#8527=DIRECTION ( 'NONE',  ( -0.9730401042858036753, 0.2306359803922028995, 5.958148513035547083E-17 ) ) ;
#8541=PRODUCT_DEFINITION_SHAPE ( 'NONE', 'NONE',  #4882 ) ;
#8547=VERTEX_POINT ( 'NONE', #7223 ) ;
#8558=DIRECTION ( 'NONE',  ( 0.000000000000000000, 1.000000000000000000, -5.551115123125781913E-15 ) ) ;
#8579=CARTESIAN_POINT ( 'NONE',  ( 27.73073027566760018, -1.721531772300955110, 13.00000000000000000 ) ) ;
#8581=CARTESIAN_POINT ( 'NONE',  ( 27.03882233449100170, -4.640652085158330387, 20.00000000000000000 ) ) ;
#8592=CARTESIAN_POINT ( 'NONE',  ( 39.27359436029389883, 22.26288585089439920, 12.99999999999979927 ) ) ;
#8596=DIRECTION ( 'NONE',  ( -0.2306359803922033158, -0.9730401042858034533, 0.000000000000000000 ) ) ;
#8602=AXIS2_PLACEMENT_3D ( 'NONE', #16057, #19864, #14268 ) ;
#8613=ORIENTED_EDGE ( 'NONE', *, *, #4840, .F. ) ;
#8626=EDGE_LOOP ( 'NONE', ( #3932, #20876, #19346, #15081 ) ) ;
#8643=EDGE_CURVE ( 'NONE', #10115, #10197, #9597, .T. ) ;
#8669=ORIENTED_EDGE ( 'NONE', *, *, #16798, .T. ) ;
#8671=EDGE_CURVE ( 'NONE', #19719, #12125, #18752, .T. ) ;
#8690=DIRECTION ( 'NONE',  ( -0.2306359803922026497, -0.9730401042858035643, 0.000000000000000000 ) ) ;
#8695=CARTESIAN_POINT ( 'NONE',  ( 36.07092311366588433, 11.78608357701207865, -19.56700000000001083 ) ) ;
#8702=FACE_BOUND ( 'NONE', #19882, .T. ) ;
#8712=CARTESIAN_POINT ( 'NONE',  ( 37.65496927852454689, 9.564447054075163379, 8.996924156394143779 ) ) ;
#8744=CARTESIAN_POINT ( 'NONE',  ( 34.74610186630083319, 11.66463240636609555, -8.849039310734035269 ) ) ;
#8768=EDGE_CURVE ( 'NONE', #18548, #19937, #15749, .T. ) ;
#8784=ORIENTED_EDGE ( 'NONE', *, *, #2230, .T. ) ;
#8790=DIRECTION ( 'NONE',  ( -0.2306359803922033991, -0.9730401042858033422, 0.000000000000000000 ) ) ;
#8796=CARTESIAN_POINT ( 'NONE',  ( 26.11627841292220253, -8.532812502301538871, 20.00000000000000000 ) ) ;
#8825=PLANE ( 'NONE',  #8602 ) ;
#8828=FACE_BOUND ( 'NONE', #18665, .T. ) ;
#8871=DIRECTION ( 'NONE',  ( 0.2306359803922028162, 0.9730401042858035643, -1.412237191019910621E-17 ) ) ;
#8899=ORIENTED_EDGE ( 'NONE', *, *, #1508, .T. ) ;
#8910=ORIENTED_EDGE ( 'NONE', *, *, #94, .F. ) ;
#8924=VECTOR ( 'NONE', #22645, 1000.000000000000000 ) ;
#8953=ORIENTED_EDGE ( 'NONE', *, *, #1683, .T. ) ;
#8962=EDGE_CURVE ( 'NONE', #20542, #199, #11937, .T. ) ;
#8990=ADVANCED_FACE ( 'NONE', ( #17880, #5750 ), #3378, .F. ) ;
#9026=AXIS2_PLACEMENT_3D ( 'NONE', #5164, #23324, #7082 ) ;
#9074=VECTOR ( 'NONE', #11492, 999.9999999999998863 ) ;
#9090=CARTESIAN_POINT ( 'NONE',  ( 35.34171762861019772, 30.38879166913039853, -20.00000000000029843 ) ) ;
#9128=ORIENTED_EDGE ( 'NONE', *, *, #1945, .T. ) ;
#9146=CIRCLE ( 'NONE', #3833, 5.000000000000004441 ) ;
#9150=DIRECTION ( 'NONE',  ( -0.9730401042858035643, 0.2306359803922028717, 5.958148513035547083E-17 ) ) ;
#9183=CARTESIAN_POINT ( 'NONE',  ( 33.90629338714457930, 8.574134987387148854, 8.864716985163932250 ) ) ;
#9202=CARTESIAN_POINT ( 'NONE',  ( 32.57408586390383221, 18.71231041770096226, 12.99999999999979927 ) ) ;
#9219=LINE ( 'NONE', #21794, #10606 ) ;
#9228=CARTESIAN_POINT ( 'NONE',  ( 36.07092311366589854, 11.78608357701213905, -8.759424124907058129 ) ) ;
#9244=DIRECTION ( 'NONE',  ( -0.9730401042858035643, 0.2306359803922028717, 5.958148513035547083E-17 ) ) ;
#9290=DIRECTION ( 'NONE',  ( -0.2306359803922033436, -0.9730401042858034533, 0.000000000000000000 ) ) ;
#9293=VECTOR ( 'NONE', #13518, 1000.000000000000000 ) ;
#9301=CARTESIAN_POINT ( 'NONE',  ( 35.11747397072458199, 7.763535785894707608, 8.759424124906642461 ) ) ;
#9308=ORIENTED_EDGE ( 'NONE', *, *, #19831, .F. ) ;
#9322=CARTESIAN_POINT ( 'NONE',  ( 30.50389457288209982, -2.378844316418859517, -13.00000000000000000 ) ) ;
#9326=CARTESIAN_POINT ( 'NONE',  ( 35.59419854219520118, 9.774809681453518806, 19.78350000000000009 ) ) ;
#9353=EDGE_CURVE ( 'NONE', #20776, #3781, #3318, .T. ) ;
#9368=CARTESIAN_POINT ( 'NONE',  ( 36.82688237244705221, -6.703751863008963419, 13.00000000000000355 ) ) ;
#9409=AXIS2_PLACEMENT_3D ( 'NONE', #2657, #393, #5751 ) ;
#9410=CARTESIAN_POINT ( 'NONE',  ( 38.09538026460411686, -1.352031289437131356, -12.99999999999999645 ) ) ;
#9426=VERTEX_POINT ( 'NONE', #7404 ) ;
#9429=AXIS2_PLACEMENT_3D ( 'NONE', #6367, #11975, #21195 ) ;
#9432=DIRECTION ( 'NONE',  ( 5.899155740360661039E-30, 4.861311874477930828E-15, 1.000000000000000000 ) ) ;
#9444=CLOSED_SHELL ( 'NONE', ( #9922, #9632, #14478, #14279, #11038, #7823, #10827, #15591, #13447, #19048, #3838, #1974, #3423, #11917, #21979, #7094, #13997, #17089, #18931, #21284, #6288, #19107, #12311, #6225, #17819, #1134, #1571, #21671, #11109, #18047, #6163, #2472, #6314, #2453, #7504, #16699, #4932, #2517, #8990, #16441 ) ) ;
#9457=EDGE_LOOP ( 'NONE', ( #21075, #11644, #76, #6880 ) ) ;
#9507=VERTEX_POINT ( 'NONE', #5606 ) ;
#9549=DIRECTION ( 'NONE',  ( -0.2306359803922033436, -0.9730401042858034533, 0.000000000000000000 ) ) ;
#9588=CARTESIAN_POINT ( 'NONE',  ( 37.18843686696352790, 8.452164511700056337, -8.953813951970682083 ) ) ;
#9597=LINE ( 'NONE', #11381, #17973 ) ;
#9600=CYLINDRICAL_SURFACE ( 'NONE', #2976, 5.000000000000000888 ) ;
#9606=LINE ( 'NONE', #4239, #18470 ) ;
#9614=VECTOR ( 'NONE', #15802, 999.9999999999998863 ) ;
#9632=ADVANCED_FACE ( 'NONE', ( #15100 ), #5957, .F. ) ;
#9644=DIRECTION ( 'NONE',  ( -0.9730401042858035643, 0.2306359803922028717, 5.958148513035547083E-17 ) ) ;
#9664=VERTEX_POINT ( 'NONE', #13215 ) ;
#9671=ORIENTED_EDGE ( 'NONE', *, *, #2161, .F. ) ;
#9701=EDGE_CURVE ( 'NONE', #3422, #9426, #361, .T. ) ;
#9705=ORIENTED_EDGE ( 'NONE', *, *, #10589, .T. ) ;
#9708=ORIENTED_EDGE ( 'NONE', *, *, #21896, .T. ) ;
#9710=ORIENTED_EDGE ( 'NONE', *, *, #16745, .F. ) ;
#9713=CARTESIAN_POINT ( 'NONE',  ( 37.21329654006962784, 11.08746082399636101, -8.849422422067901195 ) ) ;
#9722=CARTESIAN_POINT ( 'NONE',  ( 36.82688237244700247, -6.703751863009053125, -12.99999999999999645 ) ) ;
#9753=ORIENTED_EDGE ( 'NONE', *, *, #385, .T. ) ;
#9757=ORIENTED_EDGE ( 'NONE', *, *, #8671, .T. ) ;
#9777=ORIENTED_EDGE ( 'NONE', *, *, #1729, .T. ) ;
#9841=VERTEX_POINT ( 'NONE', #836 ) ;
#9856=EDGE_LOOP ( 'NONE', ( #5881, #3420, #19141, #19026 ) ) ;
#9861=EDGE_LOOP ( 'NONE', ( #280, #10472, #11089, #9891 ) ) ;
#9869=EDGE_LOOP ( 'NONE', ( #20231, #716, #23259, #10791 ) ) ;
#9885=DIRECTION ( 'NONE',  ( -0.1630842657209329583, -0.6880432561069529385, 0.7071067811865517916 ) ) ;
#9888=DIRECTION ( 'NONE',  ( -0.2306359803922009288, -0.9730401042858040084, 0.000000000000000000 ) ) ;
#9891=ORIENTED_EDGE ( 'NONE', *, *, #13044, .T. ) ;
#9904=CARTESIAN_POINT ( 'NONE',  ( 36.50043006307940630, 22.92019839501199741, -13.00000000000030020 ) ) ;
#9914=DIRECTION ( 'NONE',  ( -0.9730401042858035643, 0.2306359803922028717, 5.958148513035547083E-17 ) ) ;
#9922=ADVANCED_FACE ( 'NONE', ( #10715, #21599 ), #16148, .F. ) ;
#9989=EDGE_LOOP ( 'NONE', ( #21085, #13878 ) ) ;
#10013=CYLINDRICAL_SURFACE ( 'NONE', #3274, 2.067000000000000171 ) ;
#10014=VECTOR ( 'NONE', #3841, 999.9999999999998863 ) ;
#10018=DIRECTION ( 'NONE',  ( 0.1630842657209349289, 0.6880432561069608211, 0.7071067811865437980 ) ) ;
#10029=AXIS2_PLACEMENT_3D ( 'NONE', #6925, #10144, #21049 ) ;
#10030=CARTESIAN_POINT ( 'NONE',  ( 36.07092311366588433, 11.78608357701227760, 19.56699999999998951 ) ) ;
#10048=AXIS2_PLACEMENT_3D ( 'NONE', #1949, #10782, #22010 ) ;
#10049=CARTESIAN_POINT ( 'NONE',  ( 35.24899100468473989, 7.732362805529279903, 8.759424124906640685 ) ) ;
#10062=DIRECTION ( 'NONE',  ( 0.1630842657209343738, 0.6880432561069577124, -0.7071067811865469066 ) ) ;
#10073=EDGE_LOOP ( 'NONE', ( #13153, #1816 ) ) ;
#10115=VERTEX_POINT ( 'NONE', #18859 ) ;
#10119=CARTESIAN_POINT ( 'NONE',  ( 35.59419854219520118, 9.774809681453239918, -37.44562646538079775 ) ) ;
#10144=DIRECTION ( 'NONE',  ( -0.9730401042858035643, 0.2306359803922028717, 5.958148513035547083E-17 ) ) ;
#10161=CARTESIAN_POINT ( 'NONE',  ( 37.66475682276774251, 9.836590499361282269, 8.984920035094594581 ) ) ;
#10169=ORIENTED_EDGE ( 'NONE', *, *, #5050, .T. ) ;
#10197=VERTEX_POINT ( 'NONE', #22744 ) ;
#10198=CARTESIAN_POINT ( 'NONE',  ( 33.69273454209145768, 8.920130599203270449, -8.912036319352662161 ) ) ;
#10233=CIRCLE ( 'NONE', #3424, 5.000000000000002665 ) ;
#10242=ORIENTED_EDGE ( 'NONE', *, *, #4811, .T. ) ;
#10290=EDGE_CURVE ( 'NONE', #1981, #14140, #1600, .T. ) ;
#10312=CARTESIAN_POINT ( 'NONE',  ( 35.80338916065181820, 11.83562432877527471, -8.762640180330977913 ) ) ;
#10339=ORIENTED_EDGE ( 'NONE', *, *, #4811, .F. ) ;
#10352=LINE ( 'NONE', #4986, #6546 ) ;
#10391=VECTOR ( 'NONE', #6291, 999.9999999999998863 ) ;
#10393=AXIS2_PLACEMENT_3D ( 'NONE', #19642, #3252, #3365 ) ;
#10402=CARTESIAN_POINT ( 'NONE',  ( 83.62762864230479920, -14.97056015138839946, -13.00000000000000000 ) ) ;
#10442=ORIENTED_EDGE ( 'NONE', *, *, #12767, .F. ) ;
#10472=ORIENTED_EDGE ( 'NONE', *, *, #10719, .F. ) ;
#10496=LINE ( 'NONE', #15580, #2632 ) ;
#10567=EDGE_CURVE ( 'NONE', #11059, #14140, #9146, .T. ) ;
#10576=EDGE_CURVE ( 'NONE', #3272, #2287, #15590, .T. ) ;
#10589=EDGE_CURVE ( 'NONE', #12554, #18732, #14454, .T. ) ;
#10606=VECTOR ( 'NONE', #7553, 1000.000000000000000 ) ;
#10629=EDGE_LOOP ( 'NONE', ( #23112, #9757, #4289, #13210 ) ) ;
#10644=CARTESIAN_POINT ( 'NONE',  ( 34.41917370704145185, 26.49663125198719982, -20.00000000000029843 ) ) ;
#10652=CARTESIAN_POINT ( 'NONE',  ( 30.72899802076640086, 10.92798958341530025, -1.881607274541729715E-15 ) ) ;
#10665=EDGE_LOOP ( 'NONE', ( #13184, #15956 ) ) ;
#10715=FACE_BOUND ( 'NONE', #12893, .T. ) ;
#10719=EDGE_CURVE ( 'NONE', #13532, #13022, #22352, .T. ) ;
#10782=DIRECTION ( 'NONE',  ( 5.899155740360660338E-30, 4.861311874477930828E-15, 1.000000000000000000 ) ) ;
#10783=AXIS2_PLACEMENT_3D ( 'NONE', #9090, #11006, #18013 ) ;
#10791=ORIENTED_EDGE ( 'NONE', *, *, #14071, .F. ) ;
#10822=ADVANCED_BREP_SHAPE_REPRESENTATION ( '', ( #17344, #12739 ), #19347 ) ;
#10827=ADVANCED_FACE ( 'NONE', ( #12180 ), #19404, .F. ) ;
#10839=AXIS2_PLACEMENT_3D ( 'NONE', #11758, #16716, #7825 ) ;
#10840=CARTESIAN_POINT ( 'NONE',  ( 35.11747397072451804, 7.763535785894483787, -37.44562646538079065 ) ) ;
#10856=DIRECTION ( 'NONE',  ( -0.9730401042858035643, 0.2306359803922028717, 5.958148513035547083E-17 ) ) ;
#10874=CARTESIAN_POINT ( 'NONE',  ( 34.28553241885766312, 11.38049369541048783, 8.912006346179969896 ) ) ;
#10886=CARTESIAN_POINT ( 'NONE',  ( 34.41917370704150159, 26.49663125198739877, 19.99999999999975131 ) ) ;
#10896=CARTESIAN_POINT ( 'NONE',  ( 40.45939906362439586, 8.621629779493279244, -2.477422125845284522E-15 ) ) ;
#10900=VERTEX_POINT ( 'NONE', #19879 ) ;
#10903=ORIENTED_EDGE ( 'NONE', *, *, #15197, .F. ) ;
#10910=ORIENTED_EDGE ( 'NONE', *, *, #19429, .T. ) ;
#10944=FACE_OUTER_BOUND ( 'NONE', #12964, .T. ) ;
#10971=CIRCLE ( 'NONE', #18928, 2.750000000000001776 ) ;
#10983=ORIENTED_EDGE ( 'NONE', *, *, #7330, .F. ) ;
#11006=DIRECTION ( 'NONE',  ( -1.239096229992449859E-15, -4.969341027244109908E-15, -1.000000000000000000 ) ) ;
#11033=VECTOR ( 'NONE', #16747, 999.9999999999998863 ) ;
#11038=ADVANCED_FACE ( 'NONE', ( #7988 ), #2519, .F. ) ;
#11045=ORIENTED_EDGE ( 'NONE', *, *, #1508, .F. ) ;
#11059=VERTEX_POINT ( 'NONE', #2408 ) ;
#11081=FACE_OUTER_BOUND ( 'NONE', #18137, .T. ) ;
#11089=ORIENTED_EDGE ( 'NONE', *, *, #14071, .T. ) ;
#11105=CIRCLE ( 'NONE', #829, 2.750000000000001776 ) ;
#11109=ADVANCED_FACE ( 'NONE', ( #13101 ), #17121, .F. ) ;
#11112=FACE_OUTER_BOUND ( 'NONE', #8626, .T. ) ;
#11133=LINE ( 'NONE', #21662, #16063 ) ;
#11150=CARTESIAN_POINT ( 'NONE',  ( 35.38043770193282711, 7.701206496806046964, -8.759424124906630027 ) ) ;
#11183=DIRECTION ( 'NONE',  ( 6.123230159571619958E-17, 0.000000000000000000, 1.000000000000000000 ) ) ;
#11228=ORIENTED_EDGE ( 'NONE', *, *, #20372, .T. ) ;
#11233=DIRECTION ( 'NONE',  ( -0.9730401042858036753, 0.2306359803922028995, 5.958148513035547083E-17 ) ) ;
#11235=CARTESIAN_POINT ( 'NONE',  ( 40.45939906362439586, 8.621629779493279244, -2.477422125845284522E-15 ) ) ;
#11244=EDGE_CURVE ( 'NONE', #9664, #13560, #18497, .T. ) ;
#11267=VERTEX_POINT ( 'NONE', #11799 ) ;
#11277=DIRECTION ( 'NONE',  ( -0.9730401042858035643, 0.2306359803922028717, 5.958148513035547083E-17 ) ) ;
#11293=LINE ( 'NONE', #18521, #854 ) ;
#11316=EDGE_LOOP ( 'NONE', ( #12039, #21323, #1407, #15016 ) ) ;
#11347=VERTEX_POINT ( 'NONE', #2873 ) ;
#11353=DIRECTION ( 'NONE',  ( -0.9730401042858035643, 0.2306359803922028717, 5.958148513035547083E-17 ) ) ;
#11370=LINE ( 'NONE', #4219, #9074 ) ;
#11376=CARTESIAN_POINT ( 'NONE',  ( 36.33263316300890011, 11.71018393288660953, -8.762640023735206896 ) ) ;
#11378=FACE_OUTER_BOUND ( 'NONE', #21474, .T. ) ;
#11381=CARTESIAN_POINT ( 'NONE',  ( 32.80472184429622473, 19.68535052198753377, -2.008708621733521550E-15 ) ) ;
#11382=AXIS2_PLACEMENT_3D ( 'NONE', #9904, #15350, #9549 ) ;
#11388=DIRECTION ( 'NONE',  ( -0.2306359803922033436, -0.9730401042858034533, 0.000000000000000000 ) ) ;
#11399=FACE_BOUND ( 'NONE', #7606, .T. ) ;
#11464=LINE ( 'NONE', #374, #19092 ) ;
#11469=CARTESIAN_POINT ( 'NONE',  ( 35.59419854219520118, 9.774809681453518806, 19.56700000000000017 ) ) ;
#11484=PLANE ( 'NONE',  #9409 ) ;
#11492=DIRECTION ( 'NONE',  ( -0.9730401042858036753, 0.2306359803922028995, 5.958148513035547083E-17 ) ) ;
#11515=CARTESIAN_POINT ( 'NONE',  ( 35.59419854219520118, 9.774809681453319854, -20.00000000000000000 ) ) ;
#11530=DIRECTION ( 'NONE',  ( -0.9730401042858035643, 0.2306359803922028717, 5.958148513035547083E-17 ) ) ;
#11536=CIRCLE ( 'NONE', #16802, 2.750000000000002220 ) ;
#11548=VECTOR ( 'NONE', #19722, 1000.000000000000000 ) ;
#11552=DIRECTION ( 'NONE',  ( 0.9730401042858035643, -0.2306359803922028717, -5.958148513035547083E-17 ) ) ;
#11575=DIRECTION ( 'NONE',  ( -0.9730401042858035643, 0.2306359803922028717, 5.958148513035547083E-17 ) ) ;
#11617=EDGE_CURVE ( 'NONE', #11726, #6764, #22269, .T. ) ;
#11630=AXIS2_PLACEMENT_3D ( 'NONE', #9322, #7197, #23328 ) ;
#11644=ORIENTED_EDGE ( 'NONE', *, *, #21381, .F. ) ;
#11670=DIRECTION ( 'NONE',  ( -0.9730401042858035643, 0.2306359803922028717, 5.958148513035547083E-17 ) ) ;
#11706=CIRCLE ( 'NONE', #23037, 2.500000000000000444 ) ;
#11710=CARTESIAN_POINT ( 'NONE',  ( 39.27359436029389883, 22.26288585089424998, -13.00000000000030020 ) ) ;
#11726=VERTEX_POINT ( 'NONE', #14835 ) ;
#11758=CARTESIAN_POINT ( 'NONE',  ( 30.72899802076640086, 10.92798958341530025, -1.881607274541729715E-15 ) ) ;
#11778=LINE ( 'NONE', #8311, #21970 ) ;
#11786=CARTESIAN_POINT ( 'NONE',  ( 40.42677426225490933, 27.12808637232325282, -13.00000000000030020 ) ) ;
#11799=CARTESIAN_POINT ( 'NONE',  ( 34.43023877205762062, 1.829043660892390566, -13.00000000000000000 ) ) ;
#11801=AXIS2_PLACEMENT_3D ( 'NONE', #8592, #10856, #3234 ) ;
#11816=CARTESIAN_POINT ( 'NONE',  ( 35.59419854219520118, 9.774809681453319854, -19.56700000000000017 ) ) ;
#11834=ORIENTED_EDGE ( 'NONE', *, *, #9701, .T. ) ;
#11847=VECTOR ( 'NONE', #5134, 999.9999999999998863 ) ;
#11877=DIRECTION ( 'NONE',  ( -0.9730401042858035643, 0.2306359803922028717, 5.958148513035547083E-17 ) ) ;
#11893=ORIENTED_EDGE ( 'NONE', *, *, #18710, .F. ) ;
#11917=ADVANCED_FACE ( 'NONE', ( #11378 ), #3997, .T. ) ;
#11937=CIRCLE ( 'NONE', #10048, 2.500000000000000444 ) ;
#11975=DIRECTION ( 'NONE',  ( -0.9730401042858035643, 0.2306359803922028717, 5.958148513035547083E-17 ) ) ;
#11983=DIRECTION ( 'NONE',  ( 1.213490492418610097E-15, 4.861311874477940294E-15, 1.000000000000000000 ) ) ;
#11993=DIRECTION ( 'NONE',  ( -0.2306359803922032603, -0.9730401042858034533, 0.000000000000000000 ) ) ;
#12014=DIRECTION ( 'NONE',  ( -1.239096229992449859E-15, -4.969341027244109908E-15, -1.000000000000000000 ) ) ;
#12017=CIRCLE ( 'NONE', #4400, 2.750000000000002220 ) ;
#12039=ORIENTED_EDGE ( 'NONE', *, *, #16620, .F. ) ;
#12056=AXIS2_PLACEMENT_3D ( 'NONE', #16636, #18806, #717 ) ;
#12060=CARTESIAN_POINT ( 'NONE',  ( 36.07092311366584880, 11.78608357701223852, 8.759424124907040365 ) ) ;
#12061=CARTESIAN_POINT ( 'NONE',  ( 34.88044566782581057, 28.44271146055880806, -13.00000000000030020 ) ) ;
#12075=AXIS2_PLACEMENT_3D ( 'NONE', #580, #11552, #7838 ) ;
#12118=ORIENTED_EDGE ( 'NONE', *, *, #9353, .T. ) ;
#12120=PLANE ( 'NONE',  #22528 ) ;
#12121=CARTESIAN_POINT ( 'NONE',  ( 33.72726576586484981, 23.57751093913000062, 12.99999999999979927 ) ) ;
#12122=EDGE_LOOP ( 'NONE', ( #6832, #7074 ) ) ;
#12124=DIRECTION ( 'NONE',  ( 1.213490492418610097E-15, 4.861311874477940294E-15, 1.000000000000000000 ) ) ;
#12125=VERTEX_POINT ( 'NONE', #15385 ) ;
#12136=EDGE_CURVE ( 'NONE', #14652, #17862, #3350, .T. ) ;
#12164=DIRECTION ( 'NONE',  ( 0.9730401042858037863, -0.2306359803922024276, -5.958148513035918094E-17 ) ) ;
#12176=CARTESIAN_POINT ( 'NONE',  ( 35.38564976618402369, 7.713890031107105472, 8.762651562745531919 ) ) ;
#12180=FACE_OUTER_BOUND ( 'NONE', #21554, .T. ) ;
#12213=CARTESIAN_POINT ( 'NONE',  ( 36.07092311366589854, 11.78608357701213905, -8.759424124907058129 ) ) ;
#12280=VERTEX_POINT ( 'NONE', #6976 ) ;
#12283=FACE_OUTER_BOUND ( 'NONE', #5489, .T. ) ;
#12291=CIRCLE ( 'NONE', #22873, 2.066999999999999282 ) ;
#12297=CARTESIAN_POINT ( 'NONE',  ( 37.01658734137052420, 11.28063437484922815, 8.819862741542941365 ) ) ;
#12311=ADVANCED_FACE ( 'NONE', ( #23438 ), #20007, .F. ) ;
#12339=CARTESIAN_POINT ( 'NONE',  ( 35.84667945578014780, -10.83917230622359895, 16.00000000000000000 ) ) ;
#12355=ORIENTED_EDGE ( 'NONE', *, *, #2964, .T. ) ;
#12382=VERTEX_POINT ( 'NONE', #9202 ) ;
#12397=DIRECTION ( 'NONE',  ( 0.9730401042858035643, -0.2306359803922028717, -5.958148513035547083E-17 ) ) ;
#12409=FACE_OUTER_BOUND ( 'NONE', #18457, .T. ) ;
#12424=EDGE_CURVE ( 'NONE', #21792, #142, #22236, .T. ) ;
#12456=VECTOR ( 'NONE', #737, 999.9999999999998863 ) ;
#12501=CARTESIAN_POINT ( 'NONE',  ( 33.27705887009660302, -3.036156860536619817, -13.00000000000000000 ) ) ;
#12502=CARTESIAN_POINT ( 'NONE',  ( 90.25841307858055984, 13.00434284682846098, -13.00000000000030020 ) ) ;
#12532=LINE ( 'NONE', #19649, #20754 ) ;
#12554=VERTEX_POINT ( 'NONE', #3843 ) ;
#12561=CARTESIAN_POINT ( 'NONE',  ( 84.26187758838335640, -12.29469986460233599, 13.00000000000000000 ) ) ;
#12575=CARTESIAN_POINT ( 'NONE',  ( 36.50043006307940630, 22.92019839501219991, 12.99999999999979927 ) ) ;
#12598=VECTOR ( 'NONE', #7485, 1000.000000000000000 ) ;
#12625=DIRECTION ( 'NONE',  ( 0.9730401042858035643, -0.2306359803922031215, -4.456532139458528310E-16 ) ) ;
#12654=CONICAL_SURFACE ( 'NONE', #10393, 2.283500000000000529, 0.7853981633974539411 ) ;
#12672=PLANE ( 'NONE',  #10783 ) ;
#12684=AXIS2_PLACEMENT_3D ( 'NONE', #694, #15190, #22659 ) ;
#12692=EDGE_CURVE ( 'NONE', #6798, #6743, #23431, .T. ) ;
#12693=EDGE_CURVE ( 'NONE', #1981, #22224, #298, .T. ) ;
#12697=DIRECTION ( 'NONE',  ( 0.1630842657209342073, 0.6880432561069562691, 0.7071067811865482389 ) ) ;
#12708=DIRECTION ( 'NONE',  ( -0.2306359803922033158, -0.9730401042858034533, 0.000000000000000000 ) ) ;
#12723=VECTOR ( 'NONE', #13873, 999.9999999999998863 ) ;
#12739=AXIS2_PLACEMENT_3D ( 'NONE', #2569, #13380, #415 ) ;
#12752=CARTESIAN_POINT ( 'NONE',  ( 33.61053995400052941, 9.178437802375466248, 8.940674882554530356 ) ) ;
#12767=EDGE_CURVE ( 'NONE', #14140, #11059, #20792, .T. ) ;
#12804=CARTESIAN_POINT ( 'NONE',  ( 35.59419854219520118, 9.774809681453319854, -19.78350000000000009 ) ) ;
#12846=LINE ( 'NONE', #20323, #11033 ) ;
#12892=AXIS2_PLACEMENT_3D ( 'NONE', #2550, #8017, #20714 ) ;
#12893=EDGE_LOOP ( 'NONE', ( #13139, #19700 ) ) ;
#12900=CARTESIAN_POINT ( 'NONE',  ( 36.20426423164212792, 11.75447824097759231, -8.759424124907058129 ) ) ;
#12927=CARTESIAN_POINT ( 'NONE',  ( 39.27359436029389883, 22.26288585089424998, -13.00000000000030020 ) ) ;
#12940=AXIS2_PLACEMENT_3D ( 'NONE', #17026, #8142, #4343 ) ;
#12964=EDGE_LOOP ( 'NONE', ( #18064, #22898, #7151, #19239 ) ) ;
#12980=CARTESIAN_POINT ( 'NONE',  ( 33.70449598666325386, 8.926526082478684287, 8.911899047890422310 ) ) ;
#13007=CARTESIAN_POINT ( 'NONE',  ( 31.65707447484311743, 2.486356205010289866, 13.00000000000000000 ) ) ;
#13016=CIRCLE ( 'NONE', #22870, 5.000000000000004441 ) ;
#13022=VERTEX_POINT ( 'NONE', #9410 ) ;
#13044=EDGE_CURVE ( 'NONE', #2445, #1396, #10971, .T. ) ;
#13062=EDGE_CURVE ( 'NONE', #22391, #20016, #3409, .T. ) ;
#13101=FACE_OUTER_BOUND ( 'NONE', #1285, .T. ) ;
#13108=EDGE_LOOP ( 'NONE', ( #21475, #22305, #9710, #17034 ) ) ;
#13120=LINE ( 'NONE', #270, #1629 ) ;
#13131=CIRCLE ( 'NONE', #17684, 2.750000000000001332 ) ;
#13139=ORIENTED_EDGE ( 'NONE', *, *, #22024, .T. ) ;
#13141=CARTESIAN_POINT ( 'NONE',  ( 37.66476571482293423, 9.834146374661965950, -8.985048276826022473 ) ) ;
#13144=CIRCLE ( 'NONE', #18850, 2.750000000000002220 ) ;
#13153=ORIENTED_EDGE ( 'NONE', *, *, #15197, .T. ) ;
#13177=CARTESIAN_POINT ( 'NONE',  ( 35.84667945578009807, -10.83917230622375882, -20.00000000000000000 ) ) ;
#13184=ORIENTED_EDGE ( 'NONE', *, *, #13522, .F. ) ;
#13204=EDGE_CURVE ( 'NONE', #21046, #19719, #22564, .T. ) ;
#13210=ORIENTED_EDGE ( 'NONE', *, *, #1560, .T. ) ;
#13215=CARTESIAN_POINT ( 'NONE',  ( 28.88391017762861424, 3.143668749128058604, 13.00000000000000000 ) ) ;
#13220=ORIENTED_EDGE ( 'NONE', *, *, #10567, .F. ) ;
#13325=DIRECTION ( 'NONE',  ( -0.1630842657209355673, -0.6880432561069612651, -0.7071067811865432429 ) ) ;
#13347=DIRECTION ( 'NONE',  ( 0.000000000000000000, 1.000000000000000000, -5.035481788031372371E-15 ) ) ;
#13378=CARTESIAN_POINT ( 'NONE',  ( 37.02539408398538257, 11.29029616550548454, -8.817835639223822852 ) ) ;
#13380=DIRECTION ( 'NONE',  ( 0.000000000000000000, 0.000000000000000000, 1.000000000000000000 ) ) ;
#13382=CARTESIAN_POINT ( 'NONE',  ( 34.88044566782589584, 28.44271146055899990, 17.99999999999970157 ) ) ;
#13393=CARTESIAN_POINT ( 'NONE',  ( 34.85554549375144973, 7.839538622613233976, -8.762651562745512379 ) ) ;
#13421=ORIENTED_EDGE ( 'NONE', *, *, #6741, .T. ) ;
#13432=CARTESIAN_POINT ( 'NONE',  ( 30.50389457288209982, -2.378844316418729843, 13.00000000000000000 ) ) ;
#13447=ADVANCED_FACE ( 'NONE', ( #2463 ), #9600, .F. ) ;
#13483=CIRCLE ( 'NONE', #10839, 9.000000000000003553 ) ;
#13518=DIRECTION ( 'NONE',  ( 1.239096229992445915E-15, 4.969341027244109908E-15, 1.000000000000000000 ) ) ;
#13522=EDGE_CURVE ( 'NONE', #11347, #8547, #11706, .T. ) ;
#13532=VERTEX_POINT ( 'NONE', #9722 ) ;
#13560=VERTEX_POINT ( 'NONE', #20631 ) ;
#13563=EDGE_CURVE ( 'NONE', #13022, #1396, #768, .T. ) ;
#13618=ORIENTED_EDGE ( 'NONE', *, *, #4421, .T. ) ;
#13652=AXIS2_PLACEMENT_3D ( 'NONE', #586, #4282, #6054 ) ;
#13739=CARTESIAN_POINT ( 'NONE',  ( 35.12900133326353114, 11.79332846112002997, -8.806536740235884508 ) ) ;
#13759=AXIS2_PLACEMENT_3D ( 'NONE', #16269, #9150, #16387 ) ;
#13777=ORIENTED_EDGE ( 'NONE', *, *, #5598, .T. ) ;
#13812=ORIENTED_EDGE ( 'NONE', *, *, #20388, .F. ) ;
#13827=CARTESIAN_POINT ( 'NONE',  ( 37.59139506199680625, 10.37158478572834142, 8.943038809424253444 ) ) ;
#13873=DIRECTION ( 'NONE',  ( -0.9730401042858036753, 0.2306359803922028995, 5.958148513035547083E-17 ) ) ;
#13877=EDGE_CURVE ( 'NONE', #10197, #6181, #19260, .T. ) ;
#13878=ORIENTED_EDGE ( 'NONE', *, *, #1144, .T. ) ;
#13909=ORIENTED_EDGE ( 'NONE', *, *, #7121, .F. ) ;
#13919=VECTOR ( 'NONE', #11983, 1000.000000000000000 ) ;
#13949=ORIENTED_EDGE ( 'NONE', *, *, #10290, .T. ) ;
#13970=AXIS2_PLACEMENT_3D ( 'NONE', #8243, #21059, #4789 ) ;
#13997=ADVANCED_FACE ( 'NONE', ( #18936 ), #11484, .T. ) ;
#14001=CARTESIAN_POINT ( 'NONE',  ( 33.27705887009660302, -3.036156860536499913, 13.00000000000000000 ) ) ;
#14015=EDGE_CURVE ( 'NONE', #9841, #9664, #18719, .T. ) ;
#14029=ORIENTED_EDGE ( 'NONE', *, *, #18904, .F. ) ;
#14041=CARTESIAN_POINT ( 'NONE',  ( 27.03882233449090222, -4.640652085158520457, -20.00000000000000000 ) ) ;
#14042=CIRCLE ( 'NONE', #3782, 2.500000000000000444 ) ;
#14051=CARTESIAN_POINT ( 'NONE',  ( 36.56346929822891667, 7.944129105593864537, 8.864692334380281480 ) ) ;
#14071=EDGE_CURVE ( 'NONE', #13532, #2445, #7654, .T. ) ;
#14080=DIRECTION ( 'NONE',  ( 0.1630842657209355673, 0.6880432561069612651, 0.7071067811865432429 ) ) ;
#14131=CIRCLE ( 'NONE', #23221, 2.750000000000002220 ) ;
#14133=CARTESIAN_POINT ( 'NONE',  ( 33.27705887009660302, -3.036156860536515012, 13.00000000000000000 ) ) ;
#14140=VERTEX_POINT ( 'NONE', #12061 ) ;
#14152=DIRECTION ( 'NONE',  ( -0.9730401042858035643, 0.2306359803922028717, 5.958148513035547083E-17 ) ) ;
#14254=AXIS2_PLACEMENT_3D ( 'NONE', #6107, #4092, #394 ) ;
#14257=FACE_BOUND ( 'NONE', #14442, .T. ) ;
#14268=DIRECTION ( 'NONE',  ( -0.9730401042858034533, 0.2306359803922031215, 0.000000000000000000 ) ) ;
#14270=DIRECTION ( 'NONE',  ( 0.2306359803922028995, 0.9730401042858036753, -5.121148285185918258E-15 ) ) ;
#14274=CARTESIAN_POINT ( 'NONE',  ( 33.72726576586480007, 23.57751093912980167, -13.00000000000030020 ) ) ;
#14279=ADVANCED_FACE ( 'NONE', ( #21062 ), #5033, .F. ) ;
#14329=ORIENTED_EDGE ( 'NONE', *, *, #14892, .F. ) ;
#14354=ORIENTED_EDGE ( 'NONE', *, *, #1097, .F. ) ;
#14389=CARTESIAN_POINT ( 'NONE',  ( 35.84667945578019754, -10.83917230622355987, 20.00000000000000000 ) ) ;
#14401=CARTESIAN_POINT ( 'NONE',  ( 35.80298882477688949, 11.83572350794559114, 8.762640023735183803 ) ) ;
#14410=AXIS2_PLACEMENT_3D ( 'NONE', #5580, #3453, #3683 ) ;
#14419=DIRECTION ( 'NONE',  ( 0.9730401042858035643, -0.2306359803922028717, -5.958148513035547083E-17 ) ) ;
#14442=EDGE_LOOP ( 'NONE', ( #17308, #15982 ) ) ;
#14454=CIRCLE ( 'NONE', #12940, 5.000000000000000888 ) ;
#14478=ADVANCED_FACE ( 'NONE', ( #23179 ), #6946, .F. ) ;
#14504=AXIS2_PLACEMENT_3D ( 'NONE', #1020, #11530, #18767 ) ;
#14526=DIRECTION ( 'NONE',  ( 0.000000000000000000, -1.000000000000000000, 5.551115123125781913E-15 ) ) ;
#14529=ORIENTED_EDGE ( 'NONE', *, *, #13522, .T. ) ;
#14531=CARTESIAN_POINT ( 'NONE',  ( 33.65811390067847242, 10.51125079953912334, 8.996926784497372154 ) ) ;
#14546=DIRECTION ( 'NONE',  ( 0.9730401042858032312, -0.2306359803922040375, 1.121193430162474340E-15 ) ) ;
#14561=DIRECTION ( 'NONE',  ( 1.213490492418603984E-15, 4.861311874477930828E-15, 1.000000000000000000 ) ) ;
#14564=DIRECTION ( 'NONE',  ( -0.2306359803922033158, -0.9730401042858034533, 0.000000000000000000 ) ) ;
#14585=FACE_OUTER_BOUND ( 'NONE', #8022, .T. ) ;
#14611=B_SPLINE_CURVE_WITH_KNOTS ( 'NONE', 3,
 ( #16189, #7176, #14401, #18335, #21638, #5380, #1808, #3605, #10874, #16295, #18, #7292, #17861, #14531, #7524, #5612, #21769, #5503, #12752, #12980, #1924, #9183, #16418, #20228, #144, #21874, #2054, #9301 ),
 .UNSPECIFIED., .F., .F.,
 ( 4, 2, 2, 2, 2, 2, 2, 2, 2, 2, 2, 2, 2, 4 ),
 ( 0.000000000000000000, 0.0004072576943254697392, 0.0008145153886509394784, 0.001629030777301878957, 0.002036288471627348967, 0.002443546165952819194, 0.002850803860278289421, 0.003258061554603759648, 0.004072576943254694465, 0.004479834637580166860, 0.004887092331905638389, 0.005294350026231110784, 0.005701607720556582312, 0.006516123109207543583 ),
 .UNSPECIFIED. ) ;
#14646=ORIENTED_EDGE ( 'NONE', *, *, #12136, .T. ) ;
#14652=VERTEX_POINT ( 'NONE', #2046 ) ;
#14677=AXIS2_PLACEMENT_3D ( 'NONE', #5850, #18685, #4310 ) ;
#14688=VECTOR ( 'NONE', #22521, 999.9999999999998863 ) ;
#14690=AXIS2_PLACEMENT_3D ( 'NONE', #21728, #106, #23274 ) ;
#14724=ORIENTED_EDGE ( 'NONE', *, *, #12136, .F. ) ;
#14738=DIRECTION ( 'NONE',  ( -0.2306359803922033991, -0.9730401042858034533, 0.000000000000000000 ) ) ;
#14777=CARTESIAN_POINT ( 'NONE',  ( 89.62416413250200264, 10.32848256004250054, -13.00000000000030020 ) ) ;
#14781=CIRCLE ( 'NONE', #19350, 5.000000000000004441 ) ;
#14782=CARTESIAN_POINT ( 'NONE',  ( 36.07092311366584880, 11.78608357701223852, 8.759424124907040365 ) ) ;
#14806=ORIENTED_EDGE ( 'NONE', *, *, #5050, .F. ) ;
#14835=CARTESIAN_POINT ( 'NONE',  ( 28.88391017762856450, 3.143668749127940920, -13.00000000000000000 ) ) ;
#14845=ORIENTED_EDGE ( 'NONE', *, *, #21771, .F. ) ;
#14865=CARTESIAN_POINT ( 'NONE',  ( 30.50389457288209982, -2.378844316418859517, -13.00000000000000000 ) ) ;
#14892=EDGE_CURVE ( 'NONE', #18732, #12554, #4831, .T. ) ;
#14919=CARTESIAN_POINT ( 'NONE',  ( 37.42446263180998756, 10.74467201676272943, -8.896276805998382997 ) ) ;
#14935=CARTESIAN_POINT ( 'NONE',  ( 35.34171762861030430, 30.38879166913060104, 15.99999999999969802 ) ) ;
#15016=ORIENTED_EDGE ( 'NONE', *, *, #23206, .F. ) ;
#15031=CIRCLE ( 'NONE', #2901, 2.500000000000000444 ) ;
#15058=CARTESIAN_POINT ( 'NONE',  ( 40.45939906362420402, 8.621629779492399948, -1.858156152378089715E-13 ) ) ;
#15071=AXIS2_PLACEMENT_3D ( 'NONE', #11816, #15470, #13347 ) ;
#15076=FACE_BOUND ( 'NONE', #16351, .T. ) ;
#15081=ORIENTED_EDGE ( 'NONE', *, *, #1670, .T. ) ;
#15100=FACE_OUTER_BOUND ( 'NONE', #7211, .T. ) ;
#15123=EDGE_CURVE ( 'NONE', #4764, #9507, #5824, .T. ) ;
#15130=EDGE_LOOP ( 'NONE', ( #538, #21669, #21675, #20082, #17341, #18545, #18245, #2315 ) ) ;
#15136=DIRECTION ( 'NONE',  ( -0.9730401042858035643, 0.2306359803922028717, 5.958148513035547083E-17 ) ) ;
#15140=CARTESIAN_POINT ( 'NONE',  ( 35.34171762861030430, 30.38879166913060104, 19.99999999999969802 ) ) ;
#15146=DIRECTION ( 'NONE',  ( -0.9730401042858036753, 0.2306359803922028995, -2.355138688025664352E-16 ) ) ;
#15149=CARTESIAN_POINT ( 'NONE',  ( 36.50043006307940630, 22.92019839501219991, 12.99999999999979927 ) ) ;
#15177=DIRECTION ( 'NONE',  ( 0.000000000000000000, -1.000000000000000000, 5.035481788031372371E-15 ) ) ;
#15190=DIRECTION ( 'NONE',  ( 1.213490492418610097E-15, 4.861311874477940294E-15, 1.000000000000000000 ) ) ;
#15197=EDGE_CURVE ( 'NONE', #22534, #1573, #6124, .T. ) ;
#15200=ORIENTED_EDGE ( 'NONE', *, *, #5113, .T. ) ;
#15208=FACE_OUTER_BOUND ( 'NONE', #9856, .T. ) ;
#15210=VECTOR ( 'NONE', #12697, 1000.000000000000114 ) ;
#15279=AXIS2_PLACEMENT_3D ( 'NONE', #6118, #6246, #993 ) ;
#15317=CARTESIAN_POINT ( 'NONE',  ( 35.34725016111838869, 18.05499787358298036, -13.00000000000030020 ) ) ;
#15341=EDGE_LOOP ( 'NONE', ( #14354, #1985, #21707, #942 ) ) ;
#15350=DIRECTION ( 'NONE',  ( -0.9730401042858035643, 0.2306359803922028717, 5.958148513035547083E-17 ) ) ;
#15385=CARTESIAN_POINT ( 'NONE',  ( 26.11627841292215280, -8.532812502301730717, -16.00000000000000000 ) ) ;
#15388=EDGE_LOOP ( 'NONE', ( #3427, #8953 ) ) ;
#15389=CARTESIAN_POINT ( 'NONE',  ( 84.26187758838335640, -12.29469986460243724, -13.00000000000000000 ) ) ;
#15440=AXIS2_PLACEMENT_3D ( 'NONE', #11235, #11353, #18704 ) ;
#15450=VECTOR ( 'NONE', #14546, 1000.000000000000227 ) ;
#15470=DIRECTION ( 'NONE',  ( 1.227507208848341976E-15, 4.920447605136010024E-15, 1.000000000000000000 ) ) ;
#15480=CARTESIAN_POINT ( 'NONE',  ( 37.63682253917825449, 9.430584805299272233, 8.999987531128503804 ) ) ;
#15553=DIRECTION ( 'NONE',  ( 0.9730401042858036753, -0.2306359803922028995, -3.393930153960344319E-16 ) ) ;
#15555=VECTOR ( 'NONE', #13325, 999.9999999999998863 ) ;
#15580=CARTESIAN_POINT ( 'NONE',  ( 35.06754128096959988, 7.552872603316687083, -19.78349999999998943 ) ) ;
#15590=CIRCLE ( 'NONE', #1169, 2.750000000000001332 ) ;
#15591=ADVANCED_FACE ( 'NONE', ( #2661 ), #189, .F. ) ;
#15601=DIRECTION ( 'NONE',  ( -0.2306359803922026497, -0.9730401042858035643, 0.000000000000000000 ) ) ;
#15632=DESIGN_CONTEXT ( 'detailed design', #22467, 'design' ) ;
#15636=CARTESIAN_POINT ( 'NONE',  ( 34.99900037908246020, 11.75885530842037241, -8.819862741542964457 ) ) ;
#15654=LINE ( 'NONE', #3061, #8924 ) ;
#15660=ORIENTED_EDGE ( 'NONE', *, *, #1412, .F. ) ;
#15732=DIRECTION ( 'NONE',  ( 1.213490492418610097E-15, 4.861311874477940294E-15, 1.000000000000000000 ) ) ;
#15746=EDGE_CURVE ( 'NONE', #645, #4600, #7666, .T. ) ;
#15749=LINE ( 'NONE', #1359, #6996 ) ;
#15755=CARTESIAN_POINT ( 'NONE',  ( 33.84066803019035063, 10.87741165379667585, -8.976009386856679484 ) ) ;
#15802=DIRECTION ( 'NONE',  ( -0.2306359803922028995, -0.9730401042858036753, 4.730251413307818851E-15 ) ) ;
#15807=ORIENTED_EDGE ( 'NONE', *, *, #2230, .F. ) ;
#15811=DIRECTION ( 'NONE',  ( -0.9730401042858038974, 0.2306359803922014562, -1.121193430162461718E-15 ) ) ;
#15830=AXIS2_PLACEMENT_3D ( 'NONE', #14865, #6315, #5961 ) ;
#15836=CARTESIAN_POINT ( 'NONE',  ( 36.90976272218952658, 8.157610693807670899, 8.912036319352676372 ) ) ;
#15851=ORIENTED_EDGE ( 'NONE', *, *, #14015, .F. ) ;
#15866=CARTESIAN_POINT ( 'NONE',  ( 36.07092311366587722, 11.78608357701199694, -37.44562646538080486 ) ) ;
#15902=ORIENTED_EDGE ( 'NONE', *, *, #8140, .T. ) ;
#15921=LINE ( 'NONE', #7036, #5462 ) ;
#15944=CARTESIAN_POINT ( 'NONE',  ( 36.20429989730508424, 11.75446978728179559, 8.759424124907038589 ) ) ;
#15956=ORIENTED_EDGE ( 'NONE', *, *, #5261, .F. ) ;
#15971=AXIS2_PLACEMENT_3D ( 'NONE', #21927, #11277, #18509 ) ;
#15980=CARTESIAN_POINT ( 'NONE',  ( 35.53353590478442214, 11.84532598660267233, -8.774845639078000303 ) ) ;
#15982=ORIENTED_EDGE ( 'NONE', *, *, #11617, .T. ) ;
#16003=AXIS2_PLACEMENT_3D ( 'NONE', #9326, #14561, #18239 ) ;
#16039=ORIENTED_EDGE ( 'NONE', *, *, #3383, .T. ) ;
#16046=ORIENTED_EDGE ( 'NONE', *, *, #20324, .F. ) ;
#16057=CARTESIAN_POINT ( 'NONE',  ( 26.11627841292210306, -8.532812502301741375, -20.00000000000000000 ) ) ;
#16063=VECTOR ( 'NONE', #16216, 999.9999999999998863 ) ;
#16081=ORIENTED_EDGE ( 'NONE', *, *, #12693, .F. ) ;
#16130=ORIENTED_EDGE ( 'NONE', *, *, #13062, .T. ) ;
#16148=CYLINDRICAL_SURFACE ( 'NONE', #6871, 9.000000000000001776 ) ;
#16155=ORIENTED_EDGE ( 'NONE', *, *, #7347, .T. ) ;
#16169=AXIS2_PLACEMENT_3D ( 'NONE', #12575, #7689, #11388 ) ;
#16189=CARTESIAN_POINT ( 'NONE',  ( 36.07092311366584880, 11.78608357701223852, 8.759424124907040365 ) ) ;
#16195=VERTEX_POINT ( 'NONE', #18690 ) ;
#16216=DIRECTION ( 'NONE',  ( -0.9730401042858036753, 0.2306359803922028995, 1.292536702527485292E-16 ) ) ;
#16269=CARTESIAN_POINT ( 'NONE',  ( 30.72899802076620190, 10.92798958341440141, -1.853207297523799892E-13 ) ) ;
#16295=CARTESIAN_POINT ( 'NONE',  ( 34.08722126974237199, 11.19602313317669307, 8.940971698096578990 ) ) ;
#16304=LINE ( 'NONE', #7531, #4290 ) ;
#16320=CYLINDRICAL_SURFACE ( 'NONE', #19570, 2.750000000000000000 ) ;
#16340=AXIS2_PLACEMENT_3D ( 'NONE', #12804, #20039, #4007 ) ;
#16351=EDGE_LOOP ( 'NONE', ( #9671, #14806 ) ) ;
#16374=EDGE_CURVE ( 'NONE', #19937, #3422, #1314, .T. ) ;
#16387=DIRECTION ( 'NONE',  ( 6.123230159571619958E-17, 0.000000000000000000, 1.000000000000000000 ) ) ;
#16395=EDGE_LOOP ( 'NONE', ( #2131, #20318, #17913, #21528 ) ) ;
#16418=CARTESIAN_POINT ( 'NONE',  ( 33.98758127650715721, 8.467323122883840369, 8.849131568618506805 ) ) ;
#16426=CARTESIAN_POINT ( 'NONE',  ( 33.91130781617516732, -0.3602965737505582910, 13.00000000000000355 ) ) ;
#16433=DIRECTION ( 'NONE',  ( -0.2306359803922026497, -0.9730401042858035643, 0.000000000000000000 ) ) ;
#16440=CARTESIAN_POINT ( 'NONE',  ( 32.64280992401804582, -5.712017147322579369, -12.99999999999999645 ) ) ;
#16441=ADVANCED_FACE ( 'NONE', ( #3579, #19851, #3787, #14257, #20063, #7383 ), #1664, .T. ) ;
#16458=CARTESIAN_POINT ( 'NONE',  ( 36.44304717685047024, 7.885313416653864316, -8.849131568618497923 ) ) ;
#16461=ORIENTED_EDGE ( 'NONE', *, *, #2678, .F. ) ;
#16498=CARTESIAN_POINT ( 'NONE',  ( 32.64280992401804582, -5.712017147322479005, 13.00000000000000355 ) ) ;
#16501=CARTESIAN_POINT ( 'NONE',  ( 39.27359436029389883, 22.26288585089424998, -13.00000000000030020 ) ) ;
#16526=ORIENTED_EDGE ( 'NONE', *, *, #20324, .T. ) ;
#16535=CARTESIAN_POINT ( 'NONE',  ( 35.11747397072458199, 7.763535785894707608, 8.759424124906642461 ) ) ;
#16564=DIRECTION ( 'NONE',  ( -2.196377653365445055E-14, -1.228149275973193960E-30, -1.000000000000000000 ) ) ;
#16567=EDGE_LOOP ( 'NONE', ( #16155, #6775 ) ) ;
#16585=ORIENTED_EDGE ( 'NONE', *, *, #16745, .T. ) ;
#16617=CARTESIAN_POINT ( 'NONE',  ( 34.41917370704150159, 26.49663125198739877, 19.99999999999975131 ) ) ;
#16620=EDGE_CURVE ( 'NONE', #1573, #22534, #11536, .T. ) ;
#16636=CARTESIAN_POINT ( 'NONE',  ( 89.62416413250210212, 10.32848256004259824, 12.99999999999970157 ) ) ;
#16641=ORIENTED_EDGE ( 'NONE', *, *, #517, .F. ) ;
#16674=EDGE_LOOP ( 'NONE', ( #23194, #1310 ) ) ;
#16699=ADVANCED_FACE ( 'NONE', ( #18425, #15076 ), #16974, .T. ) ;
#16704=VERTEX_POINT ( 'NONE', #16498 ) ;
#16716=DIRECTION ( 'NONE',  ( 0.9730401042858035643, -0.2306359803922028717, -5.958148513035547083E-17 ) ) ;
#16731=ORIENTED_EDGE ( 'NONE', *, *, #4840, .T. ) ;
#16745=EDGE_CURVE ( 'NONE', #12382, #4733, #13016, .T. ) ;
#16747=DIRECTION ( 'NONE',  ( -0.1630842657209349289, -0.6880432561069608211, -0.7071067811865437980 ) ) ;
#16798=EDGE_CURVE ( 'NONE', #22224, #11059, #2957, .T. ) ;
#16802=AXIS2_PLACEMENT_3D ( 'NONE', #4035, #9644, #2494 ) ;
#16818=CARTESIAN_POINT ( 'NONE',  ( 36.90212305349054844, 8.168604748878864896, -8.911899047890418757 ) ) ;
#16824=ORIENTED_EDGE ( 'NONE', *, *, #17411, .F. ) ;
#16828=DIRECTION ( 'NONE',  ( -0.9730401042858035643, 0.2306359803922028717, 5.958148513035547083E-17 ) ) ;
#16845=FACE_BOUND ( 'NONE', #10073, .T. ) ;
#16853=DIRECTION ( 'NONE',  ( -0.9730401042858035643, 0.2306359803922028717, 5.958148513035547083E-17 ) ) ;
#16860=DIRECTION ( 'NONE',  ( -0.2306359803922026497, -0.9730401042858035643, 0.000000000000000000 ) ) ;
#16865=DIRECTION ( 'NONE',  ( -0.2306359803922033436, -0.9730401042858034533, 0.000000000000000000 ) ) ;
#16880=EDGE_LOOP ( 'NONE', ( #5213, #10339, #8669, #10442 ) ) ;
#16898=PLANE ( 'NONE',  #22265 ) ;
#16909=DIRECTION ( 'NONE',  ( -0.9730401042858036753, 0.2306359803922028995, 5.958148513035547083E-17 ) ) ;
#16926=CARTESIAN_POINT ( 'NONE',  ( 37.48433000560739714, 10.62229491794307279, -8.912006346179977001 ) ) ;
#16969=EDGE_LOOP ( 'NONE', ( #17373, #5325, #16461, #13909 ) ) ;
#16974=PLANE ( 'NONE',  #20607 ) ;
#17010=CARTESIAN_POINT ( 'NONE',  ( 29.35071467092108577, -7.244044837847749108, 13.00000000000000000 ) ) ;
#17024=CARTESIAN_POINT ( 'NONE',  ( 82.99337969622625621, -17.64642043817435990, -13.00000000000000000 ) ) ;
#17026=CARTESIAN_POINT ( 'NONE',  ( 39.27359436029389883, 22.26288585089444894, 12.99999999999979927 ) ) ;
#17034=ORIENTED_EDGE ( 'NONE', *, *, #5598, .F. ) ;
#17089=ADVANCED_FACE ( 'NONE', ( #3513, #3855 ), #12672, .T. ) ;
#17100=EDGE_CURVE ( 'NONE', #4764, #21792, #11133, .T. ) ;
#17109=CARTESIAN_POINT ( 'NONE',  ( 28.65327419723657343, 2.170628644843063615, -6.523238081173185874E-16 ) ) ;
#17121=CYLINDRICAL_SURFACE ( 'NONE', #12056, 2.750000000000000000 ) ;
#17135=DIRECTION ( 'NONE',  ( 0.000000000000000000, -1.000000000000000000, 5.035481788031372371E-15 ) ) ;
#17160=DIRECTION ( 'NONE',  ( -0.1630842657209350399, -0.6880432561069612651, -0.7071067811865433539 ) ) ;
#17286=CARTESIAN_POINT ( 'NONE',  ( 90.25841307858064511, 13.00434284682856045, 12.99999999999970157 ) ) ;
#17289=CARTESIAN_POINT ( 'NONE',  ( 37.46113131852559519, -4.027891576222994985, 13.00000000000000000 ) ) ;
#17308=ORIENTED_EDGE ( 'NONE', *, *, #2678, .T. ) ;
#17309=CARTESIAN_POINT ( 'NONE',  ( 35.93754633002667731, 11.81769736674259086, -8.759424124907059905 ) ) ;
#17341=ORIENTED_EDGE ( 'NONE', *, *, #13204, .F. ) ;
#17344=MANIFOLD_SOLID_BREP ( 'Imported1', #9444 ) ;
#17345=VERTEX_POINT ( 'NONE', #396 ) ;
#17373=ORIENTED_EDGE ( 'NONE', *, *, #19989, .F. ) ;
#17393=CARTESIAN_POINT ( 'NONE',  ( 37.28322146592795150, 10.97386708096955665, 8.864945788362589951 ) ) ;
#17411=EDGE_CURVE ( 'NONE', #20776, #16195, #22138, .T. ) ;
#17417=ORIENTED_EDGE ( 'NONE', *, *, #8671, .F. ) ;
#17421=CARTESIAN_POINT ( 'NONE',  ( 33.90636897763663882, 8.573931448519822140, -8.864692334380263716 ) ) ;
#17504=EDGE_CURVE ( 'NONE', #21288, #4764, #15921, .T. ) ;
#17506=DIRECTION ( 'NONE',  ( -0.9730401042858035643, 0.2306359803922028717, 5.958148513035547083E-17 ) ) ;
#17570=AXIS2_PLACEMENT_3D ( 'NONE', #23205, #14419, #16433 ) ;
#17639=FACE_OUTER_BOUND ( 'NONE', #18696, .T. ) ;
#17665=CARTESIAN_POINT ( 'NONE',  ( 34.27363088173783723, 8.178923185754959135, -8.806404184311304562 ) ) ;
#17673=CARTESIAN_POINT ( 'NONE',  ( 35.34171762861025456, 30.38879166913045182, -16.00000000000029843 ) ) ;
#17676=CARTESIAN_POINT ( 'NONE',  ( 33.27705887009660302, -3.036156860536499913, 13.00000000000000000 ) ) ;
#17684=AXIS2_PLACEMENT_3D ( 'NONE', #14133, #1522, #8790 ) ;
#17691=CARTESIAN_POINT ( 'NONE',  ( 39.27359436029389883, 22.26288585089429972, -13.00000000000030020 ) ) ;
#17711=( NAMED_UNIT ( * ) PLANE_ANGLE_UNIT ( ) SI_UNIT ( $, .RADIAN. ) );
#17754=AXIS2_PLACEMENT_3D ( 'NONE', #8579, #2981, #8690 ) ;
#17775=ORIENTED_EDGE ( 'NONE', *, *, #16798, .F. ) ;
#17786=DIRECTION ( 'NONE',  ( -0.9730401042858036753, 0.2306359803922028995, 5.958148513035547083E-17 ) ) ;
#17819=ADVANCED_FACE ( 'NONE', ( #4503 ), #22546, .F. ) ;
#17829=DIRECTION ( 'NONE',  ( 0.1630842657209334579, 0.6880432561069538266, -0.7071067811865507924 ) ) ;
#17845=CARTESIAN_POINT ( 'NONE',  ( 44.09191575480142689, 23.94701142199386368, 12.99999999999970512 ) ) ;
#17861=CARTESIAN_POINT ( 'NONE',  ( 33.77054299527826942, 10.75717911589417319, 8.985048276826017144 ) ) ;
#17862=VERTEX_POINT ( 'NONE', #8307 ) ;
#17880=FACE_OUTER_BOUND ( 'NONE', #9457, .T. ) ;
#17911=CIRCLE ( 'NONE', #14504, 5.000000000000002665 ) ;
#17913=ORIENTED_EDGE ( 'NONE', *, *, #7347, .F. ) ;
#17932=VECTOR ( 'NONE', #15811, 1000.000000000000114 ) ;
#17942=( NAMED_UNIT ( * ) SI_UNIT ( $, .STERADIAN. ) SOLID_ANGLE_UNIT ( ) );
#17950=DIRECTION ( 'NONE',  ( 0.9730401042858035643, -0.2306359803922028717, -5.958148513035547083E-17 ) ) ;
#17973=VECTOR ( 'NONE', #8158, 999.9999999999998863 ) ;
#17986=AXIS2_PLACEMENT_3D ( 'NONE', #10652, #1596, #8871 ) ;
#17991=UNCERTAINTY_MEASURE_WITH_UNIT (LENGTH_MEASURE( 1.000000000000000082E-05 ), #3210, 'distance_accuracy_value', 'NONE');
#17998=VERTEX_POINT ( 'NONE', #19470 ) ;
#18013=DIRECTION ( 'NONE',  ( 0.000000000000000000, -1.000000000000000000, 4.969341027244109908E-15 ) ) ;
#18018=VECTOR ( 'NONE', #12625, 1000.000000000000114 ) ;
#18040=ORIENTED_EDGE ( 'NONE', *, *, #5273, .T. ) ;
#18047=ADVANCED_FACE ( 'NONE', ( #7122, #3198 ), #12120, .T. ) ;
#18064=ORIENTED_EDGE ( 'NONE', *, *, #21314, .F. ) ;
#18069=ORIENTED_EDGE ( 'NONE', *, *, #1560, .F. ) ;
#18108=CARTESIAN_POINT ( 'NONE',  ( 38.12041445833288122, 17.39768532946521162, -13.00000000000030020 ) ) ;
#18127=EDGE_CURVE ( 'NONE', #645, #7554, #21818, .T. ) ;
#18137=EDGE_LOOP ( 'NONE', ( #17417, #5378, #6485, #4512 ) ) ;
#18239=DIRECTION ( 'NONE',  ( -0.2306359803922033713, -0.9730401042858034533, 4.558064749665356219E-15 ) ) ;
#18245=ORIENTED_EDGE ( 'NONE', *, *, #1729, .F. ) ;
#18252=CARTESIAN_POINT ( 'NONE',  ( 36.79306370352710331, 8.085618792784300624, -8.896078739569128757 ) ) ;
#18291=CARTESIAN_POINT ( 'NONE',  ( 89.62416413250200264, 10.32848256004250054, -13.00000000000030020 ) ) ;
#18310=ORIENTED_EDGE ( 'NONE', *, *, #2964, .F. ) ;
#18335=CARTESIAN_POINT ( 'NONE',  ( 35.53134815212258246, 11.84531904168216343, 8.774963029737106623 ) ) ;
#18361=DIRECTION ( 'NONE',  ( -0.9730401042858035643, 0.2306359803922028717, 5.958148513035547083E-17 ) ) ;
#18362=FACE_OUTER_BOUND ( 'NONE', #15341, .T. ) ;
#18397=ORIENTED_EDGE ( 'NONE', *, *, #17504, .T. ) ;
#18425=FACE_OUTER_BOUND ( 'NONE', #3364, .T. ) ;
#18457=EDGE_LOOP ( 'NONE', ( #22577, #20200, #16526, #14529 ) ) ;
#18470=VECTOR ( 'NONE', #20857, 999.9999999999998863 ) ;
#18485=CARTESIAN_POINT ( 'NONE',  ( 32.12387896813558541, -7.901357381965519622, 13.00000000000000000 ) ) ;
#18490=CARTESIAN_POINT ( 'NONE',  ( 36.57968191736579655, 11.59683649233991964, -8.774963029737127940 ) ) ;
#18497=CIRCLE ( 'NONE', #17754, 5.000000000000001776 ) ;
#18506=ORIENTED_EDGE ( 'NONE', *, *, #5261, .T. ) ;
#18509=DIRECTION ( 'NONE',  ( -0.2306359803922032603, -0.9730401042858034533, 0.000000000000000000 ) ) ;
#18521=CARTESIAN_POINT ( 'NONE',  ( 29.35071467092108577, -7.244044837847879670, -13.00000000000000000 ) ) ;
#18545=ORIENTED_EDGE ( 'NONE', *, *, #7899, .F. ) ;
#18548=VERTEX_POINT ( 'NONE', #12339 ) ;
#18586=DIRECTION ( 'NONE',  ( -0.2306359803922009288, -0.9730401042858040084, 0.000000000000000000 ) ) ;
#18610=CARTESIAN_POINT ( 'NONE',  ( 37.65485242725145554, 9.563919128020760496, -8.996926784497379259 ) ) ;
#18614=DIRECTION ( 'NONE',  ( 0.9730401042858034533, -0.2306359803922031215, 0.000000000000000000 ) ) ;
#18638=FACE_BOUND ( 'NONE', #15388, .T. ) ;
#18665=EDGE_LOOP ( 'NONE', ( #13812, #11893 ) ) ;
#18685=DIRECTION ( 'NONE',  ( -0.9730401042858035643, 0.2306359803922028717, 5.958148513035547083E-17 ) ) ;
#18690=CARTESIAN_POINT ( 'NONE',  ( 35.11747397072451093, 7.763535785894755570, 19.56700000000001083 ) ) ;
#18696=EDGE_LOOP ( 'NONE', ( #23246, #19128, #20487, #7923 ) ) ;
#18704=DIRECTION ( 'NONE',  ( -0.2306359803922031215, -0.9730401042858033422, 0.000000000000000000 ) ) ;
#18710=EDGE_CURVE ( 'NONE', #4918, #1609, #14131, .T. ) ;
#18719=LINE ( 'NONE', #13007, #12456 ) ;
#18732=VERTEX_POINT ( 'NONE', #7437 ) ;
#18736=CARTESIAN_POINT ( 'NONE',  ( 36.12085580342079538, 11.99674675958995174, -19.78350000000001074 ) ) ;
#18752=LINE ( 'NONE', #22519, #1634 ) ;
#18754=DIRECTION ( 'NONE',  ( -1.239096229992449859E-15, -4.969341027244109908E-15, -1.000000000000000000 ) ) ;
#18767=DIRECTION ( 'NONE',  ( -0.2306359803922032603, -0.9730401042858034533, 0.000000000000000000 ) ) ;
#18806=DIRECTION ( 'NONE',  ( -0.9730401042858035643, 0.2306359803922028717, 5.958148513035547083E-17 ) ) ;
#18814=ORIENTED_EDGE ( 'NONE', *, *, #7481, .T. ) ;
#18850=AXIS2_PLACEMENT_3D ( 'NONE', #21748, #5485, #3695 ) ;
#18859=CARTESIAN_POINT ( 'NONE',  ( 32.80472184429622473, 19.68535052198753377, -2.008708621733521550E-15 ) ) ;
#18873=ORIENTED_EDGE ( 'NONE', *, *, #12424, .F. ) ;
#18903=DIRECTION ( 'NONE',  ( 0.9730401042858035643, -0.2306359803922028717, -5.958148513035547083E-17 ) ) ;
#18904=EDGE_CURVE ( 'NONE', #1573, #4918, #4563, .T. ) ;
#18907=CARTESIAN_POINT ( 'NONE',  ( 36.30795141656454916, -8.893092097652150585, -18.00000000000000000 ) ) ;
#18910=ORIENTED_EDGE ( 'NONE', *, *, #15123, .T. ) ;
#18916=ORIENTED_EDGE ( 'NONE', *, *, #13877, .F. ) ;
#18922=FACE_OUTER_BOUND ( 'NONE', #16880, .T. ) ;
#18928=AXIS2_PLACEMENT_3D ( 'NONE', #3810, #2042, #9290 ) ;
#18931=ADVANCED_FACE ( 'NONE', ( #20613 ), #6243, .T. ) ;
#18936=FACE_OUTER_BOUND ( 'NONE', #3481, .T. ) ;
#18975=LINE ( 'NONE', #785, #1984 ) ;
#19001=DIRECTION ( 'NONE',  ( -0.2306359803922031770, -0.9730401042858034533, 0.000000000000000000 ) ) ;
#19026=ORIENTED_EDGE ( 'NONE', *, *, #21896, .F. ) ;
#19029=ORIENTED_EDGE ( 'NONE', *, *, #8643, .F. ) ;
#19048=ADVANCED_FACE ( 'NONE', ( #17639 ), #21070, .F. ) ;
#19053=AXIS2_PLACEMENT_3D ( 'NONE', #1987, #9244, #7457 ) ;
#19060=DIRECTION ( 'NONE',  ( 0.9730401042858035643, -0.2306359803922028717, -5.958148513035547083E-17 ) ) ;
#19069=DIRECTION ( 'NONE',  ( -1.448479254059754007E-17, -0.7167018829406569536, 0.6973796749184170141 ) ) ;
#19085=LINE ( 'NONE', #2810, #10014 ) ;
#19092=VECTOR ( 'NONE', #20343, 999.9999999999997726 ) ;
#19107=ADVANCED_FACE ( 'NONE', ( #12409 ), #12654, .F. ) ;
#19128=ORIENTED_EDGE ( 'NONE', *, *, #17411, .T. ) ;
#19141=ORIENTED_EDGE ( 'NONE', *, *, #22024, .F. ) ;
#19170=CARTESIAN_POINT ( 'NONE',  ( 44.14957474989945041, 24.19027144806515039, -20.00000000000029843 ) ) ;
#19175=CARTESIAN_POINT ( 'NONE',  ( 37.34886511858087488, 8.673867739723879922, 8.976164948525100939 ) ) ;
#19203=LINE ( 'NONE', #15866, #13919 ) ;
#19217=LINE ( 'NONE', #8296, #12723 ) ;
#19239=ORIENTED_EDGE ( 'NONE', *, *, #20683, .F. ) ;
#19260=CIRCLE ( 'NONE', #1414, 9.000000000000005329 ) ;
#19316=CARTESIAN_POINT ( 'NONE',  ( 33.55185054466894456, 10.12066834538196147, -9.000012392934834793 ) ) ;
#19346=ORIENTED_EDGE ( 'NONE', *, *, #16374, .F. ) ;
#19347=( GEOMETRIC_REPRESENTATION_CONTEXT ( 3 ) GLOBAL_UNCERTAINTY_ASSIGNED_CONTEXT ( ( #17991 ) ) GLOBAL_UNIT_ASSIGNED_CONTEXT ( ( #3210, #17711, #17942 ) ) REPRESENTATION_CONTEXT ( 'NONE', 'WORKASPACE' ) );
#19350=AXIS2_PLACEMENT_3D ( 'NONE', #16501, #14152, #23282 ) ;
#19351=EDGE_LOOP ( 'NONE', ( #13618, #12118 ) ) ;
#19391=EDGE_CURVE ( 'NONE', #20204, #13560, #6324, .T. ) ;
#19400=CARTESIAN_POINT ( 'NONE',  ( 35.79117365064221445, 7.712783139516915298, 8.783920975641617446 ) ) ;
#19404=CYLINDRICAL_SURFACE ( 'NONE', #7860, 5.000000000000000888 ) ;
#19417=ORIENTED_EDGE ( 'NONE', *, *, #7481, .F. ) ;
#19429=EDGE_CURVE ( 'NONE', #22544, #22391, #11464, .T. ) ;
#19470=CARTESIAN_POINT ( 'NONE',  ( 28.65327419723657343, 2.170628644843063615, -6.523238081173185874E-16 ) ) ;
#19505=FACE_OUTER_BOUND ( 'NONE', #1034, .T. ) ;
#19506=LINE ( 'NONE', #12502, #11847 ) ;
#19517=CARTESIAN_POINT ( 'NONE',  ( 35.11747397072458199, 7.763535785894707608, 8.759424124906642461 ) ) ;
#19570=AXIS2_PLACEMENT_3D ( 'NONE', #14777, #5405, #22012 ) ;
#19600=DIRECTION ( 'NONE',  ( 0.2306359803922028162, 0.9730401042858035643, -1.412237191019910621E-17 ) ) ;
#19642=CARTESIAN_POINT ( 'NONE',  ( 35.59419854219520118, 9.774809681453319854, -19.78350000000000009 ) ) ;
#19649=CARTESIAN_POINT ( 'NONE',  ( 31.65707447484311743, 2.486356205010160192, -13.00000000000000000 ) ) ;
#19700=ORIENTED_EDGE ( 'NONE', *, *, #21834, .T. ) ;
#19719=VERTEX_POINT ( 'NONE', #7157 ) ;
#19722=DIRECTION ( 'NONE',  ( 1.213490492418610097E-15, 4.861311874477940294E-15, 1.000000000000000000 ) ) ;
#19781=SHAPE_REPRESENTATION ( '1602p_c_36', ( #12739 ), #19347 ) ;
#19831=EDGE_CURVE ( 'NONE', #12125, #10900, #18975, .T. ) ;
#19832=SHAPE_REPRESENTATION_RELATIONSHIP ( 'NONE' , 'NONE' ,  #19781, #10822 ) ;
#19846=VECTOR ( 'NONE', #5969, 999.9999999999998863 ) ;
#19851=FACE_BOUND ( 'NONE', #711, .T. ) ;
#19864=DIRECTION ( 'NONE',  ( -0.2306359803922031215, -0.9730401042858034533, 5.121148285185918258E-15 ) ) ;
#19879=CARTESIAN_POINT ( 'NONE',  ( 27.03882233449094841, -4.640652085158520457, -20.00000000000000000 ) ) ;
#19882=EDGE_LOOP ( 'NONE', ( #6466, #8457 ) ) ;
#19937=VERTEX_POINT ( 'NONE', #4375 ) ;
#19971=CIRCLE ( 'NONE', #1746, 9.000000000000003553 ) ;
#19989=EDGE_CURVE ( 'NONE', #11267, #17345, #17911, .T. ) ;
#20007=CYLINDRICAL_SURFACE ( 'NONE', #9026, 2.067000000000000171 ) ;
#20016=VERTEX_POINT ( 'NONE', #17673 ) ;
#20039=DIRECTION ( 'NONE',  ( -1.227507208848341976E-15, -4.920447605136010024E-15, -1.000000000000000000 ) ) ;
#20063=FACE_BOUND ( 'NONE', #16567, .T. ) ;
#20082=ORIENTED_EDGE ( 'NONE', *, *, #23018, .F. ) ;
#20116=CIRCLE ( 'NONE', #3434, 2.750000000000001332 ) ;
#20177=FACE_BOUND ( 'NONE', #9989, .T. ) ;
#20200=ORIENTED_EDGE ( 'NONE', *, *, #15746, .T. ) ;
#20204=VERTEX_POINT ( 'NONE', #18485 ) ;
#20228=CARTESIAN_POINT ( 'NONE',  ( 34.17143381353265852, 8.269326149122052882, 8.819913685435246009 ) ) ;
#20231=ORIENTED_EDGE ( 'NONE', *, *, #1683, .F. ) ;
#20255=CYLINDRICAL_SURFACE ( 'NONE', #14254, 2.750000000000000888 ) ;
#20263=ORIENTED_EDGE ( 'NONE', *, *, #23038, .F. ) ;
#20270=DIRECTION ( 'NONE',  ( 0.2306359803922028717, 0.9730401042858035643, -5.065637133954654909E-15 ) ) ;
#20300=LINE ( 'NONE', #13177, #9293 ) ;
#20303=DIRECTION ( 'NONE',  ( -0.9730401042858035643, 0.2306359803922028717, 5.958148513035547083E-17 ) ) ;
#20318=ORIENTED_EDGE ( 'NONE', *, *, #14015, .T. ) ;
#20323=CARTESIAN_POINT ( 'NONE',  ( 44.61084671068384466, 26.13635165663675153, -18.00000000000029843 ) ) ;
#20324=EDGE_CURVE ( 'NONE', #4600, #11347, #22606, .T. ) ;
#20343=DIRECTION ( 'NONE',  ( -0.9730401042858037863, 0.2306359803922024276, 5.958148513035967398E-17 ) ) ;
#20372=EDGE_CURVE ( 'NONE', #2287, #3272, #22484, .T. ) ;
#20388=EDGE_CURVE ( 'NONE', #1609, #4918, #8094, .T. ) ;
#20401=VECTOR ( 'NONE', #17786, 999.9999999999998863 ) ;
#20441=EDGE_LOOP ( 'NONE', ( #20263, #9128, #18916, #19029 ) ) ;
#20487=ORIENTED_EDGE ( 'NONE', *, *, #20877, .F. ) ;
#20489=VECTOR ( 'NONE', #12164, 999.9999999999997726 ) ;
#20536=CARTESIAN_POINT ( 'NONE',  ( 43.45766680872284837, 21.27115113520789791, 12.99999999999970157 ) ) ;
#20542=VERTEX_POINT ( 'NONE', #6719 ) ;
#20607=AXIS2_PLACEMENT_3D ( 'NONE', #696, #7960, #6176 ) ;
#20613=FACE_OUTER_BOUND ( 'NONE', #10629, .T. ) ;
#20615=ORIENTED_EDGE ( 'NONE', *, *, #17100, .F. ) ;
#20616=DIRECTION ( 'NONE',  ( -0.2306359803922033991, -0.9730401042858034533, 0.000000000000000000 ) ) ;
#20631=CARTESIAN_POINT ( 'NONE',  ( 26.57755037370658613, -6.586732293729981258, 13.00000000000000000 ) ) ;
#20652=EDGE_LOOP ( 'NONE', ( #14845, #14329, #13777, #8613 ) ) ;
#20665=EDGE_LOOP ( 'NONE', ( #8910, #14724, #3486, #8784 ) ) ;
#20682=VERTEX_POINT ( 'NONE', #16426 ) ;
#20683=EDGE_CURVE ( 'NONE', #14652, #6743, #16304, .T. ) ;
#20714=DIRECTION ( 'NONE',  ( -0.2306359803922033991, -0.9730401042858034533, 0.000000000000000000 ) ) ;
#20754=VECTOR ( 'NONE', #3493, 999.9999999999998863 ) ;
#20766=CIRCLE ( 'NONE', #8272, 5.000000000000002665 ) ;
#20773=DIRECTION ( 'NONE',  ( 0.9730401042858035643, -0.2306359803922028717, -5.958148513035547083E-17 ) ) ;
#20776=VERTEX_POINT ( 'NONE', #16535 ) ;
#20778=ORIENTED_EDGE ( 'NONE', *, *, #16374, .T. ) ;
#20792=CIRCLE ( 'NONE', #6392, 5.000000000000004441 ) ;
#20823=CARTESIAN_POINT ( 'NONE',  ( 36.44273712271338894, 7.885218776542735952, 8.849098278953681174 ) ) ;
#20857=DIRECTION ( 'NONE',  ( -0.9730401042858036753, 0.2306359803922028995, 5.958148513035547083E-17 ) ) ;
#20876=ORIENTED_EDGE ( 'NONE', *, *, #7750, .T. ) ;
#20877=EDGE_CURVE ( 'NONE', #4635, #16195, #12291, .T. ) ;
#20924=DIRECTION ( 'NONE',  ( -0.9730401042858036753, 0.2306359803922023999, 0.000000000000000000 ) ) ;
#20945=DIRECTION ( 'NONE',  ( 1.227507208848341976E-15, 4.920447605136010024E-15, 1.000000000000000000 ) ) ;
#21031=CYLINDRICAL_SURFACE ( 'NONE', #7714, 2.750000000000000888 ) ;
#21046=VERTEX_POINT ( 'NONE', #4900 ) ;
#21049=DIRECTION ( 'NONE',  ( 6.123230159571619958E-17, 0.000000000000000000, 1.000000000000000000 ) ) ;
#21058=B_SPLINE_CURVE_WITH_KNOTS ( 'NONE', 3,
 ( #2466, #773, #13393, #8044, #8283, #17665, #3277, #8397, #17421, #10198, #21091, #6626, #22980, #3169, #19316, #4945, #3041, #1259, #15755, #6987, #1130, #1479, #8744, #15636, #13739, #22876, #15980, #10312, #17309, #12213 ),
 .UNSPECIFIED., .F., .F.,
 ( 4, 2, 2, 2, 2, 2, 2, 2, 2, 2, 2, 2, 2, 2, 4 ),
 ( 0.006516123109207627717, 0.006923489735540700948, 0.007330856361873773312, 0.007738222988206846543, 0.008145589614539918907, 0.008960322867206065370, 0.009367689493539138601, 0.009775056119872211832, 0.01018242274620528506, 0.01058978937253835656, 0.01140452262520452037, 0.01181188925153760054, 0.01221925587787068071, 0.01262662250420376261, 0.01303398913053684278 ),
 .UNSPECIFIED. ) ;
#21059=DIRECTION ( 'NONE',  ( -0.9730401042858035643, 0.2306359803922028717, 5.958148513035547083E-17 ) ) ;
#21062=FACE_OUTER_BOUND ( 'NONE', #9869, .T. ) ;
#21065=CARTESIAN_POINT ( 'NONE',  ( 35.59419854219520118, 9.774809681453319854, -19.56700000000000017 ) ) ;
#21070=CYLINDRICAL_SURFACE ( 'NONE', #1983, 2.067000000000000171 ) ;
#21075=ORIENTED_EDGE ( 'NONE', *, *, #1945, .F. ) ;
#21085=ORIENTED_EDGE ( 'NONE', *, *, #13877, .T. ) ;
#21089=CARTESIAN_POINT ( 'NONE',  ( 37.65360996504041680, 27.78539891644101445, -13.00000000000030020 ) ) ;
#21091=CARTESIAN_POINT ( 'NONE',  ( 33.59715865393970091, 9.176414746571007086, -8.942923417076592330 ) ) ;
#21172=DIRECTION ( 'NONE',  ( -0.9730401042858035643, 0.2306359803922028717, 5.958148513035547083E-17 ) ) ;
#21178=EDGE_LOOP ( 'NONE', ( #20615, #18910, #7366, #692 ) ) ;
#21195=DIRECTION ( 'NONE',  ( -0.2306359803922033158, -0.9730401042858034533, 0.000000000000000000 ) ) ;
#21248=APPLICATION_CONTEXT ( 'configuration controlled 3d designs of mechanical parts and assemblies' ) ;
#21284=ADVANCED_FACE ( 'NONE', ( #11081 ), #8825, .T. ) ;
#21288=VERTEX_POINT ( 'NONE', #21507 ) ;
#21293=CARTESIAN_POINT ( 'NONE',  ( 37.52959221163365555, 9.036526310759173342, 8.996869837679785320 ) ) ;
#21314=EDGE_CURVE ( 'NONE', #17862, #14652, #13144, .T. ) ;
#21323=ORIENTED_EDGE ( 'NONE', *, *, #18904, .T. ) ;
#21332=VECTOR ( 'NONE', #2316, 999.9999999999998863 ) ;
#21357=CIRCLE ( 'NONE', #17570, 5.000000000000001776 ) ;
#21365=EDGE_LOOP ( 'NONE', ( #21741, #15660, #9708, #536 ) ) ;
#21377=AXIS2_PLACEMENT_3D ( 'NONE', #23160, #1199, #20924 ) ;
#21381=EDGE_CURVE ( 'NONE', #10115, #17998, #19971, .T. ) ;
#21474=EDGE_LOOP ( 'NONE', ( #18397, #1234, #1168, #2270 ) ) ;
#21475=ORIENTED_EDGE ( 'NONE', *, *, #10589, .F. ) ;
#21507=CARTESIAN_POINT ( 'NONE',  ( 44.14957474989950015, 24.19027144806535290, 19.99999999999975131 ) ) ;
#21528=ORIENTED_EDGE ( 'NONE', *, *, #19391, .F. ) ;
#21544=FACE_OUTER_BOUND ( 'NONE', #20665, .T. ) ;
#21546=VECTOR ( 'NONE', #9885, 1000.000000000000114 ) ;
#21554=EDGE_LOOP ( 'NONE', ( #16081, #13949, #13220, #17775 ) ) ;
#21575=FACE_OUTER_BOUND ( 'NONE', #20652, .T. ) ;
#21599=FACE_OUTER_BOUND ( 'NONE', #20441, .T. ) ;
#21621=DIRECTION ( 'NONE',  ( 0.2306359803922028995, 0.9730401042858036753, -4.730251413307818851E-15 ) ) ;
#21638=CARTESIAN_POINT ( 'NONE',  ( 35.39416599996382473, 11.83651012589115936, 8.784148981162486436 ) ) ;
#21662=CARTESIAN_POINT ( 'NONE',  ( 35.34171762861030430, 30.38879166913060104, 15.99999999999969802 ) ) ;
#21669=ORIENTED_EDGE ( 'NONE', *, *, #1670, .F. ) ;
#21671=ADVANCED_FACE ( 'NONE', ( #21575 ), #5312, .F. ) ;
#21675=ORIENTED_EDGE ( 'NONE', *, *, #8768, .F. ) ;
#21707=ORIENTED_EDGE ( 'NONE', *, *, #7121, .T. ) ;
#21728=CARTESIAN_POINT ( 'NONE',  ( 39.27359436029389883, 22.26288585089444894, 12.99999999999979927 ) ) ;
#21741=ORIENTED_EDGE ( 'NONE', *, *, #18127, .F. ) ;
#21748=CARTESIAN_POINT ( 'NONE',  ( 43.45766680872284837, 21.27115113520779843, -13.00000000000030020 ) ) ;
#21769=CARTESIAN_POINT ( 'NONE',  ( 33.51035039627143419, 9.711136848494149376, 8.987168322345956639 ) ) ;
#21771=EDGE_CURVE ( 'NONE', #12554, #4733, #9606, .T. ) ;
#21791=ORIENTED_EDGE ( 'NONE', *, *, #19391, .T. ) ;
#21792=VERTEX_POINT ( 'NONE', #14935 ) ;
#21794=CARTESIAN_POINT ( 'NONE',  ( 35.34171762861030430, 30.38879166913060104, 19.99999999999969802 ) ) ;
#21818=LINE ( 'NONE', #5800, #3497 ) ;
#21834=EDGE_CURVE ( 'NONE', #7554, #12280, #21058, .T. ) ;
#21836=SHAPE_DEFINITION_REPRESENTATION ( #8541, #19781 ) ;
#21874=CARTESIAN_POINT ( 'NONE',  ( 34.60161846897012339, 7.941814927679100578, 8.772741540512809522 ) ) ;
#21896=EDGE_CURVE ( 'NONE', #4600, #12280, #19203, .T. ) ;
#21913=CARTESIAN_POINT ( 'NONE',  ( 35.11747397072451804, 7.763535785894566388, -19.56699999999998951 ) ) ;
#21915=CARTESIAN_POINT ( 'NONE',  ( 35.65846783274012211, 7.691313958534617967, -8.772741540512798863 ) ) ;
#21918=AXIS2_PLACEMENT_3D ( 'NONE', #13382, #6255, #18614 ) ;
#21927=CARTESIAN_POINT ( 'NONE',  ( 33.27705887009660302, -3.036156860536630031, -13.00000000000000000 ) ) ;
#21930=DIRECTION ( 'NONE',  ( 1.213490492418610097E-15, 4.861311874477940294E-15, 1.000000000000000000 ) ) ;
#21960=EDGE_LOOP ( 'NONE', ( #15902, #16039, #4057, #19417 ) ) ;
#21970=VECTOR ( 'NONE', #12124, 1000.000000000000000 ) ;
#21979=ADVANCED_FACE ( 'NONE', ( #4228 ), #7910, .T. ) ;
#22006=CARTESIAN_POINT ( 'NONE',  ( 34.88044566782589584, 28.44271146055899990, 17.99999999999970157 ) ) ;
#22010=DIRECTION ( 'NONE',  ( 0.000000000000000000, -1.000000000000000000, 5.551115123125781913E-15 ) ) ;
#22012=DIRECTION ( 'NONE',  ( -0.2306359803922010121, -0.9730401042858040084, 0.000000000000000000 ) ) ;
#22021=DIRECTION ( 'NONE',  ( -0.9730401042858035643, 0.2306359803922028717, 5.958148513035547083E-17 ) ) ;
#22024=EDGE_CURVE ( 'NONE', #12280, #7554, #8317, .T. ) ;
#22053=ORIENTED_EDGE ( 'NONE', *, *, #7330, .T. ) ;
#22079=FACE_OUTER_BOUND ( 'NONE', #1105, .T. ) ;
#22088=LINE ( 'NONE', #5361, #18018 ) ;
#22122=DIRECTION ( 'NONE',  ( -1.213490492418603984E-15, -4.861311874477930828E-15, -1.000000000000000000 ) ) ;
#22137=DIRECTION ( 'NONE',  ( -0.2306359803922031770, -0.9730401042858034533, 0.000000000000000000 ) ) ;
#22138=LINE ( 'NONE', #10840, #11548 ) ;
#22151=CARTESIAN_POINT ( 'NONE',  ( 37.57874659166015618, 10.36844021841513985, -8.940971698096582543 ) ) ;
#22162=CARTESIAN_POINT ( 'NONE',  ( 30.72899802076640086, 10.92798958341530025, -1.881607274541729715E-15 ) ) ;
#22170=ORIENTED_EDGE ( 'NONE', *, *, #9701, .F. ) ;
#22224=VERTEX_POINT ( 'NONE', #18108 ) ;
#22236=LINE ( 'NONE', #22006, #2947 ) ;
#22240=AXIS2_PLACEMENT_3D ( 'NONE', #10402, #21172, #6452 ) ;
#22261=CARTESIAN_POINT ( 'NONE',  ( 37.09915056617500539, 8.351545750134603097, -8.940674882554525027 ) ) ;
#22265=AXIS2_PLACEMENT_3D ( 'NONE', #5621, #9432, #7644 ) ;
#22269=CIRCLE ( 'NONE', #12075, 5.000000000000001776 ) ;
#22305=ORIENTED_EDGE ( 'NONE', *, *, #21771, .T. ) ;
#22306=EDGE_CURVE ( 'NONE', #142, #21288, #7187, .T. ) ;
#22318=EDGE_LOOP ( 'NONE', ( #16824, #6012, #15200, #4105 ) ) ;
#22331=AXIS2_PLACEMENT_3D ( 'NONE', #4780, #6804, #1079 ) ;
#22352=CIRCLE ( 'NONE', #12892, 2.750000000000001332 ) ;
#22353=FACE_OUTER_BOUND ( 'NONE', #9861, .T. ) ;
#22361=DIRECTION ( 'NONE',  ( -0.2306359803922033991, -0.9730401042858034533, 0.000000000000000000 ) ) ;
#22367=ORIENTED_EDGE ( 'NONE', *, *, #23038, .T. ) ;
#22391=VERTEX_POINT ( 'NONE', #10644 ) ;
#22409=FACE_OUTER_BOUND ( 'NONE', #15130, .T. ) ;
#22446=DIRECTION ( 'NONE',  ( -0.2306359803922027607, -0.9730401042858035643, 0.000000000000000000 ) ) ;
#22447=DIRECTION ( 'NONE',  ( 0.2306359803922017615, 0.9730401042858037863, -3.356987858687580135E-15 ) ) ;
#22467=APPLICATION_CONTEXT ( 'configuration controlled 3d designs of mechanical parts and assemblies' ) ;
#22484=CIRCLE ( 'NONE', #2006, 2.750000000000001332 ) ;
#22497=CARTESIAN_POINT ( 'NONE',  ( 37.46113131852559519, -4.027891576222994985, 13.00000000000000000 ) ) ;
#22519=CARTESIAN_POINT ( 'NONE',  ( 26.11627841292210306, -8.532812502301720059, -16.00000000000000000 ) ) ;
#22521=DIRECTION ( 'NONE',  ( -0.9730401042858036753, 0.2306359803922028995, 5.958148513035547083E-17 ) ) ;
#22528=AXIS2_PLACEMENT_3D ( 'NONE', #17691, #1163, #4856 ) ;
#22534=VERTEX_POINT ( 'NONE', #3837 ) ;
#22544=VERTEX_POINT ( 'NONE', #19170 ) ;
#22546=CYLINDRICAL_SURFACE ( 'NONE', #12684, 2.067000000000000171 ) ;
#22550=DIRECTION ( 'NONE',  ( -0.9730401042858035643, 0.2306359803922028717, 5.958148513035547083E-17 ) ) ;
#22564=LINE ( 'NONE', #18907, #21546 ) ;
#22577=ORIENTED_EDGE ( 'NONE', *, *, #6230, .F. ) ;
#22606=LINE ( 'NONE', #18736, #3884 ) ;
#22616=AXIS2_PLACEMENT_3D ( 'NONE', #6591, #19060, #15601 ) ;
#22633=ORIENTED_EDGE ( 'NONE', *, *, #7750, .F. ) ;
#22645=DIRECTION ( 'NONE',  ( -1.239096229992445915E-15, -4.969341027244109908E-15, -1.000000000000000000 ) ) ;
#22659=DIRECTION ( 'NONE',  ( 0.2306359803922017615, 0.9730401042858037863, -3.356987858687580135E-15 ) ) ;
#22694=DIRECTION ( 'NONE',  ( -0.1630842657209360114, -0.6880432561069645958, -0.7071067811865398012 ) ) ;
#22723=LINE ( 'NONE', #5909, #15210 ) ;
#22744=CARTESIAN_POINT ( 'NONE',  ( 42.53512288715421619, 17.37899071806551277, -2.604523473037073991E-15 ) ) ;
#22765=VECTOR ( 'NONE', #14270, 999.9999999999998863 ) ;
#22784=EDGE_LOOP ( 'NONE', ( #15807, #7414 ) ) ;
#22798=DIRECTION ( 'NONE',  ( -0.9730401042858035643, 0.2306359803922028717, 5.958148513035547083E-17 ) ) ;
#22870=AXIS2_PLACEMENT_3D ( 'NONE', #12121, #20773, #19001 ) ;
#22873=AXIS2_PLACEMENT_3D ( 'NONE', #11469, #22122, #17135 ) ;
#22876=CARTESIAN_POINT ( 'NONE',  ( 35.39632699307497177, 11.83676830303470240, -8.783982963266950605 ) ) ;
#22898=ORIENTED_EDGE ( 'NONE', *, *, #94, .T. ) ;
#22943=CARTESIAN_POINT ( 'NONE',  ( 35.34171762861025456, 30.38879166913039853, -20.00000000000029843 ) ) ;
#22980=CARTESIAN_POINT ( 'NONE',  ( 33.52368772877015601, 9.713198297474395559, -8.984918777770040776 ) ) ;
#22983=ORIENTED_EDGE ( 'NONE', *, *, #20877, .T. ) ;
#23018=EDGE_CURVE ( 'NONE', #19719, #18548, #20300, .T. ) ;
#23037=AXIS2_PLACEMENT_3D ( 'NONE', #11515, #18754, #8040 ) ;
#23038=EDGE_CURVE ( 'NONE', #17998, #10115, #13483, .T. ) ;
#23063=CARTESIAN_POINT ( 'NONE',  ( 37.20029037402979100, 11.08292547562999353, 8.849039310734006847 ) ) ;
#23112=ORIENTED_EDGE ( 'NONE', *, *, #13204, .T. ) ;
#23140=EDGE_CURVE ( 'NONE', #9426, #12125, #15654, .T. ) ;
#23160=CARTESIAN_POINT ( 'NONE',  ( 26.57755037370660034, -6.586732293729940402, 18.00000000000000000 ) ) ;
#23177=CARTESIAN_POINT ( 'NONE',  ( 37.49471903941907414, 10.63079050866130970, 8.911849358505318008 ) ) ;
#23179=FACE_OUTER_BOUND ( 'NONE', #16395, .T. ) ;
#23194=ORIENTED_EDGE ( 'NONE', *, *, #10567, .T. ) ;
#23205=CARTESIAN_POINT ( 'NONE',  ( 27.73073027566760018, -1.721531772300955110, 13.00000000000000000 ) ) ;
#23206=EDGE_CURVE ( 'NONE', #22534, #1609, #19217, .T. ) ;
#23221=AXIS2_PLACEMENT_3D ( 'NONE', #1958, #22021, #14564 ) ;
#23245=ORIENTED_EDGE ( 'NONE', *, *, #14892, .T. ) ;
#23246=ORIENTED_EDGE ( 'NONE', *, *, #9353, .F. ) ;
#23259=ORIENTED_EDGE ( 'NONE', *, *, #6489, .T. ) ;
#23274=DIRECTION ( 'NONE',  ( -0.2306359803922033436, -0.9730401042858034533, 0.000000000000000000 ) ) ;
#23282=DIRECTION ( 'NONE',  ( -0.2306359803922031770, -0.9730401042858034533, 0.000000000000000000 ) ) ;
#23297=PLANE ( 'NONE',  #11801 ) ;
#23314=ORIENTED_EDGE ( 'NONE', *, *, #2161, .T. ) ;
#23324=DIRECTION ( 'NONE',  ( 1.213490492418610097E-15, 4.861311874477940294E-15, 1.000000000000000000 ) ) ;
#23328=DIRECTION ( 'NONE',  ( -0.2306359803922026497, -0.9730401042858035643, 0.000000000000000000 ) ) ;
#23335=EDGE_LOOP ( 'NONE', ( #3672, #22367 ) ) ;
#23378=MECHANICAL_CONTEXT ( 'NONE', #21248, 'mechanical' ) ;
#23409=DIRECTION ( 'NONE',  ( -0.2306359803922031770, -0.9730401042858034533, 0.000000000000000000 ) ) ;
#23431=CIRCLE ( 'NONE', #5622, 2.750000000000002220 ) ;
#23438=FACE_OUTER_BOUND ( 'NONE', #21365, .T. ) ;
#23448=VECTOR ( 'NONE', #10018, 999.9999999999998863 ) ;
#23536=COLOUR_RGB('Slate Gray', 0.40784314, 0.44705882, 0.49803922);
#23537=FILL_AREA_STYLE_COLOUR('',#23536);
#23538=FILL_AREA_STYLE('',(#23537));
#23539=SURFACE_STYLE_FILL_AREA(#23538);
#23540=SURFACE_SIDE_STYLE('',(#23539));
#23541=SURFACE_STYLE_USAGE(.BOTH.,#23540);
#23542=PRESENTATION_STYLE_ASSIGNMENT((#23541));
#23585=STYLED_ITEM('',(#23542),#17344);
#23586=MECHANICAL_DESIGN_GEOMETRIC_PRESENTATION_REPRESENTATION('',(#23585),#19347);
ENDSEC;
END-ISO-10303-21;
